ISO-10303-21;
HEADER;
/* Generated by software containing ST-Developer
 * from STEP Tools, Inc. (www.steptools.com) 
 */

FILE_DESCRIPTION(
/* description */ (''),
/* implementation_level */ '2;1');

FILE_NAME(
/* name */ '17_Hex_Nut_ISO_4032_M8.step',
/* time_stamp */ '2026-10-26T06:13:19-07:00',
/* author */ (''),
/* organization */ (''),
/* preprocessor_version */ 'ST-DEVELOPER v20.2',
/* originating_system */ 'Autodesk Translation Framework v15.15.0.0',
/* authorisation */ '');

FILE_SCHEMA (('AUTOMOTIVE_DESIGN { 1 0 10303 214 3 1 1 }','TECHNICAL_DATA_PACKAGING'));
ENDSEC;

DATA;
#10=MECHANICAL_DESIGN_GEOMETRIC_PRESENTATION_REPRESENTATION('',(#316),#56639);
#276=SHAPE_REPRESENTATION_RELATIONSHIP('SRR','None',#56764,#296);
#296=ADVANCED_BREP_SHAPE_REPRESENTATION('',(#336),#56638);
#316=STYLED_ITEM('',(#56922),#336);
#336=MANIFOLD_SOLID_BREP('Body1',#16968);
#361=B_SPLINE_SURFACE_WITH_KNOTS('',3,3,((#56136,#56137,#56138,#56139,#56140),
(#56141,#56142,#56143,#56144,#56145),(#56146,#56147,#56148,#56149,#56150),
(#56151,#56152,#56153,#56154,#56155)),.UNSPECIFIED.,.F.,.F.,.F.,(4,4),(4,
1,4),(0.,1.),(0.166194858401647,0.504344050522728,0.955209640017503),
 .UNSPECIFIED.);
#362=B_SPLINE_SURFACE_WITH_KNOTS('',3,3,((#56185,#56186,#56187,#56188,#56189),
(#56190,#56191,#56192,#56193,#56194),(#56195,#56196,#56197,#56198,#56199),
(#56200,#56201,#56202,#56203,#56204)),.UNSPECIFIED.,.F.,.F.,.F.,(4,4),(4,
1,4),(0.,1.),(0.166194858401647,0.504344050522728,0.955209640017503),
 .UNSPECIFIED.);
#363=B_SPLINE_SURFACE_WITH_KNOTS('',3,3,((#56274,#56275,#56276,#56277,#56278),
(#56279,#56280,#56281,#56282,#56283),(#56284,#56285,#56286,#56287,#56288),
(#56289,#56290,#56291,#56292,#56293)),.UNSPECIFIED.,.F.,.F.,.F.,(4,4),(4,
1,4),(0.,1.),(0.166194858401646,0.617060447896421,0.955209640017502),
 .UNSPECIFIED.);
#364=B_SPLINE_SURFACE_WITH_KNOTS('',3,3,((#56370,#56371,#56372,#56373,#56374),
(#56375,#56376,#56377,#56378,#56379),(#56380,#56381,#56382,#56383,#56384),
(#56385,#56386,#56387,#56388,#56389)),.UNSPECIFIED.,.F.,.F.,.F.,(4,4),(4,
1,4),(0.,1.),(0.166194858401647,0.617060447896421,0.955209640017502),
 .UNSPECIFIED.);
#365=B_SPLINE_SURFACE_WITH_KNOTS('',3,3,((#56403,#56404,#56405,#56406,#56407),
(#56408,#56409,#56410,#56411,#56412),(#56413,#56414,#56415,#56416,#56417),
(#56418,#56419,#56420,#56421,#56422)),.UNSPECIFIED.,.F.,.F.,.F.,(4,4),(4,
1,4),(0.,1.),(0.166194858401647,0.504344050522728,0.955209640017502),
 .UNSPECIFIED.);
#366=B_SPLINE_SURFACE_WITH_KNOTS('',3,3,((#56444,#56445,#56446,#56447,#56448),
(#56449,#56450,#56451,#56452,#56453),(#56454,#56455,#56456,#56457,#56458),
(#56459,#56460,#56461,#56462,#56463)),.UNSPECIFIED.,.F.,.F.,.F.,(4,4),(4,
1,4),(0.,1.),(0.166194858401646,0.504344050522728,0.955209640017502),
 .UNSPECIFIED.);
#562=FACE_BOUND('',#3873,.T.);
#563=FACE_BOUND('',#3900,.T.);
#652=CONICAL_SURFACE('',#18688,6.15985379710312,1.30871360570645);
#653=CONICAL_SURFACE('',#18696,7.25527674973257,1.046630884618);
#654=CONICAL_SURFACE('',#18697,7.25527674973257,1.046630884618);
#655=CONICAL_SURFACE('',#18698,7.25527674973257,1.046630884618);
#656=CONICAL_SURFACE('',#18699,7.25527674973257,1.046630884618);
#657=CONICAL_SURFACE('',#18700,7.25527674973257,1.046630884618);
#658=CONICAL_SURFACE('',#18701,7.25527674973257,1.046630884618);
#659=CONICAL_SURFACE('',#18719,7.25527674973257,1.046630884618);
#660=CONICAL_SURFACE('',#18721,4.25,0.674740942223553);
#661=CONICAL_SURFACE('',#18726,4.25,0.674740942223553);
#1214=CIRCLE('',#18689,5.90797863635533);
#1215=CIRCLE('',#18690,6.41172895785092);
#1216=CIRCLE('',#18691,6.41172895785092);
#1217=CIRCLE('',#18692,6.41172895785092);
#1218=CIRCLE('',#18693,6.41172895785092);
#1219=CIRCLE('',#18694,6.41172895785092);
#1220=CIRCLE('',#18695,6.41172895785092);
#1221=CIRCLE('',#18703,4.37);
#1222=CIRCLE('',#18720,6.17797863635533);
#1223=CIRCLE('',#18722,4.37);
#1224=CIRCLE('',#18723,4.05);
#1225=CIRCLE('',#18725,4.05);
#1760=CYLINDRICAL_SURFACE('',#18724,4.05);
#1792=(
BOUNDED_CURVE()
B_SPLINE_CURVE(2,(#56398,#56399,#56400),.UNSPECIFIED.,.F.,.F.)
B_SPLINE_CURVE_WITH_KNOTS((3,3),(0.118301700433499,0.165554978945076),
 .UNSPECIFIED.)
CURVE()
GEOMETRIC_REPRESENTATION_ITEM()
RATIONAL_B_SPLINE_CURVE((1.0089042769369,1.00941185088304,1.0089042769369))
REPRESENTATION_ITEM('')
);
#1793=(
BOUNDED_CURVE()
B_SPLINE_CURVE(2,(#56431,#56432,#56433),.UNSPECIFIED.,.F.,.F.)
B_SPLINE_CURVE_WITH_KNOTS((3,3),(0.118301700433498,0.165554978945076),
 .UNSPECIFIED.)
CURVE()
GEOMETRIC_REPRESENTATION_ITEM()
RATIONAL_B_SPLINE_CURVE((1.00890427693691,1.00941185088304,1.00890427693691))
REPRESENTATION_ITEM('')
);
#1794=(
BOUNDED_CURVE()
B_SPLINE_CURVE(2,(#56439,#56440,#56441),.UNSPECIFIED.,.F.,.F.)
B_SPLINE_CURVE_WITH_KNOTS((3,3),(0.118301700433499,0.165554978945077),
 .UNSPECIFIED.)
CURVE()
GEOMETRIC_REPRESENTATION_ITEM()
RATIONAL_B_SPLINE_CURVE((1.0089042769369,1.00941185088304,1.0089042769369))
REPRESENTATION_ITEM('')
);
#1795=(
BOUNDED_CURVE()
B_SPLINE_CURVE(2,(#56472,#56473,#56474),.UNSPECIFIED.,.F.,.F.)
B_SPLINE_CURVE_WITH_KNOTS((3,3),(0.118301700433496,0.165554978945074),
 .UNSPECIFIED.)
CURVE()
GEOMETRIC_REPRESENTATION_ITEM()
RATIONAL_B_SPLINE_CURVE((1.0089042769369,1.00941185088304,1.0089042769369))
REPRESENTATION_ITEM('')
);
#1796=(
BOUNDED_CURVE()
B_SPLINE_CURVE(2,(#56480,#56481,#56482),.UNSPECIFIED.,.F.,.F.)
B_SPLINE_CURVE_WITH_KNOTS((3,3),(0.118301700433498,0.165554978945076),
 .UNSPECIFIED.)
CURVE()
GEOMETRIC_REPRESENTATION_ITEM()
RATIONAL_B_SPLINE_CURVE((1.00890427693691,1.00941185088304,1.00890427693691))
REPRESENTATION_ITEM('')
);
#1797=(
BOUNDED_CURVE()
B_SPLINE_CURVE(2,(#56488,#56489,#56490),.UNSPECIFIED.,.F.,.F.)
B_SPLINE_CURVE_WITH_KNOTS((3,3),(0.118301700433497,0.165554978945074),
 .UNSPECIFIED.)
CURVE()
GEOMETRIC_REPRESENTATION_ITEM()
RATIONAL_B_SPLINE_CURVE((1.00890427693689,1.00941185088303,1.00890427693689))
REPRESENTATION_ITEM('')
);
#1798=(
BOUNDED_CURVE()
B_SPLINE_CURVE(2,(#56494,#56495,#56496),.UNSPECIFIED.,.F.,.F.)
B_SPLINE_CURVE_WITH_KNOTS((3,3),(0.17570560818583,0.94569889023331),
 .UNSPECIFIED.)
CURVE()
GEOMETRIC_REPRESENTATION_ITEM()
RATIONAL_B_SPLINE_CURVE((1.0815388920082,1.2270078002172,1.08153889200821))
REPRESENTATION_ITEM('')
);
#1799=(
BOUNDED_CURVE()
B_SPLINE_CURVE(2,(#56498,#56499,#56500),.UNSPECIFIED.,.F.,.F.)
B_SPLINE_CURVE_WITH_KNOTS((3,3),(0.17570560818583,0.945698890233311),
 .UNSPECIFIED.)
CURVE()
GEOMETRIC_REPRESENTATION_ITEM()
RATIONAL_B_SPLINE_CURVE((1.0815388920082,1.2270078002172,1.08153889200821))
REPRESENTATION_ITEM('')
);
#1800=(
BOUNDED_CURVE()
B_SPLINE_CURVE(2,(#56502,#56503,#56504),.UNSPECIFIED.,.F.,.F.)
B_SPLINE_CURVE_WITH_KNOTS((3,3),(0.17570560818583,0.94569889023331),
 .UNSPECIFIED.)
CURVE()
GEOMETRIC_REPRESENTATION_ITEM()
RATIONAL_B_SPLINE_CURVE((1.0815388920082,1.2270078002172,1.08153889200821))
REPRESENTATION_ITEM('')
);
#1801=(
BOUNDED_CURVE()
B_SPLINE_CURVE(2,(#56510,#56511,#56512),.UNSPECIFIED.,.F.,.F.)
B_SPLINE_CURVE_WITH_KNOTS((3,3),(0.17570560818583,0.560702249209475),
 .UNSPECIFIED.)
CURVE()
GEOMETRIC_REPRESENTATION_ITEM()
RATIONAL_B_SPLINE_CURVE((1.0815388920082,1.15427334611268,1.1542733461127))
REPRESENTATION_ITEM('')
);
#1802=(
BOUNDED_CURVE()
B_SPLINE_CURVE(2,(#56513,#56514,#56515),.UNSPECIFIED.,.F.,.F.)
B_SPLINE_CURVE_WITH_KNOTS((3,3),(0.17570560818583,0.945698890233311),
 .UNSPECIFIED.)
CURVE()
GEOMETRIC_REPRESENTATION_ITEM()
RATIONAL_B_SPLINE_CURVE((1.0815388920082,1.2270078002172,1.08153889200821))
REPRESENTATION_ITEM('')
);
#1803=(
BOUNDED_CURVE()
B_SPLINE_CURVE(2,(#56516,#56517,#56518),.UNSPECIFIED.,.F.,.F.)
B_SPLINE_CURVE_WITH_KNOTS((3,3),(0.17570560818583,0.945698890233311),
 .UNSPECIFIED.)
CURVE()
GEOMETRIC_REPRESENTATION_ITEM()
RATIONAL_B_SPLINE_CURVE((1.0815388920082,1.2270078002172,1.08153889200821))
REPRESENTATION_ITEM('')
);
#1804=(
BOUNDED_CURVE()
B_SPLINE_CURVE(2,(#56519,#56520,#56521),.UNSPECIFIED.,.F.,.F.)
B_SPLINE_CURVE_WITH_KNOTS((3,3),(0.560702249209475,0.94569889023331),
 .UNSPECIFIED.)
CURVE()
GEOMETRIC_REPRESENTATION_ITEM()
RATIONAL_B_SPLINE_CURVE((1.1542733461127,1.15427334611272,1.08153889200821))
REPRESENTATION_ITEM('')
);
#2741=FACE_OUTER_BOUND('',#3862,.T.);
#2742=FACE_OUTER_BOUND('',#3863,.T.);
#2743=FACE_OUTER_BOUND('',#3864,.T.);
#2744=FACE_OUTER_BOUND('',#3865,.T.);
#2745=FACE_OUTER_BOUND('',#3866,.T.);
#2746=FACE_OUTER_BOUND('',#3867,.T.);
#2747=FACE_OUTER_BOUND('',#3868,.T.);
#2748=FACE_OUTER_BOUND('',#3869,.T.);
#2749=FACE_OUTER_BOUND('',#3870,.T.);
#2750=FACE_OUTER_BOUND('',#3871,.T.);
#2751=FACE_OUTER_BOUND('',#3872,.T.);
#2752=FACE_OUTER_BOUND('',#3874,.T.);
#2753=FACE_OUTER_BOUND('',#3875,.T.);
#2754=FACE_OUTER_BOUND('',#3876,.T.);
#2755=FACE_OUTER_BOUND('',#3877,.T.);
#2756=FACE_OUTER_BOUND('',#3878,.T.);
#2757=FACE_OUTER_BOUND('',#3879,.T.);
#2758=FACE_OUTER_BOUND('',#3880,.T.);
#2759=FACE_OUTER_BOUND('',#3881,.T.);
#2760=FACE_OUTER_BOUND('',#3882,.T.);
#2761=FACE_OUTER_BOUND('',#3883,.T.);
#2762=FACE_OUTER_BOUND('',#3884,.T.);
#2763=FACE_OUTER_BOUND('',#3885,.T.);
#2764=FACE_OUTER_BOUND('',#3886,.T.);
#2765=FACE_OUTER_BOUND('',#3887,.T.);
#2766=FACE_OUTER_BOUND('',#3888,.T.);
#2767=FACE_OUTER_BOUND('',#3889,.T.);
#2768=FACE_OUTER_BOUND('',#3890,.T.);
#2769=FACE_OUTER_BOUND('',#3891,.T.);
#2770=FACE_OUTER_BOUND('',#3892,.T.);
#2771=FACE_OUTER_BOUND('',#3893,.T.);
#2772=FACE_OUTER_BOUND('',#3894,.T.);
#2773=FACE_OUTER_BOUND('',#3895,.T.);
#2774=FACE_OUTER_BOUND('',#3896,.T.);
#2775=FACE_OUTER_BOUND('',#3897,.T.);
#2776=FACE_OUTER_BOUND('',#3898,.T.);
#2777=FACE_OUTER_BOUND('',#3899,.T.);
#3862=EDGE_LOOP('',(#15544,#15545,#15546,#15547,#15548,#15549,#15550,#15551,
#15552,#15553,#15554,#15555,#15556,#15557,#15558,#15559));
#3863=EDGE_LOOP('',(#15560,#15561,#15562,#15563,#15564,#15565));
#3864=EDGE_LOOP('',(#15566,#15567,#15568,#15569,#15570,#15571));
#3865=EDGE_LOOP('',(#15572,#15573,#15574));
#3866=EDGE_LOOP('',(#15575,#15576,#15577));
#3867=EDGE_LOOP('',(#15578,#15579,#15580));
#3868=EDGE_LOOP('',(#15581,#15582,#15583));
#3869=EDGE_LOOP('',(#15584,#15585,#15586));
#3870=EDGE_LOOP('',(#15587,#15588,#15589));
#3871=EDGE_LOOP('',(#15590,#15591,#15592,#15593,#15594,#15595));
#3872=EDGE_LOOP('',(#15596));
#3873=EDGE_LOOP('',(#15597));
#3874=EDGE_LOOP('',(#15598,#15599,#15600));
#3875=EDGE_LOOP('',(#15601,#15602,#15603));
#3876=EDGE_LOOP('',(#15604,#15605,#15606));
#3877=EDGE_LOOP('',(#15607,#15608,#15609));
#3878=EDGE_LOOP('',(#15610,#15611,#15612));
#3879=EDGE_LOOP('',(#15613,#15614,#15615));
#3880=EDGE_LOOP('',(#15616,#15617,#15618,#15619,#15620,#15621));
#3881=EDGE_LOOP('',(#15622,#15623,#15624,#15625));
#3882=EDGE_LOOP('',(#15626,#15627,#15628,#15629,#15630,#15631,#15632));
#3883=EDGE_LOOP('',(#15633,#15634,#15635,#15636));
#3884=EDGE_LOOP('',(#15637,#15638,#15639,#15640));
#3885=EDGE_LOOP('',(#15641,#15642,#15643,#15644,#15645,#15646));
#3886=EDGE_LOOP('',(#15647,#15648,#15649,#15650));
#3887=EDGE_LOOP('',(#15651,#15652,#15653,#15654));
#3888=EDGE_LOOP('',(#15655,#15656,#15657,#15658));
#3889=EDGE_LOOP('',(#15659,#15660,#15661,#15662));
#3890=EDGE_LOOP('',(#15663,#15664,#15665,#15666));
#3891=EDGE_LOOP('',(#15667,#15668,#15669,#15670));
#3892=EDGE_LOOP('',(#15671,#15672,#15673,#15674,#15675,#15676,#15677,#15678,
#15679,#15680,#15681,#15682,#15683,#15684,#15685,#15686));
#3893=EDGE_LOOP('',(#15687,#15688,#15689,#15690));
#3894=EDGE_LOOP('',(#15691,#15692,#15693,#15694));
#3895=EDGE_LOOP('',(#15695,#15696,#15697,#15698));
#3896=EDGE_LOOP('',(#15699,#15700,#15701,#15702));
#3897=EDGE_LOOP('',(#15703,#15704,#15705,#15706,#15707));
#3898=EDGE_LOOP('',(#15708,#15709,#15710,#15711));
#3899=EDGE_LOOP('',(#15712));
#3900=EDGE_LOOP('',(#15713));
#4832=LINE('',#55927,#5786);
#4833=LINE('',#56317,#5787);
#4834=LINE('',#56326,#5788);
#4835=LINE('',#56328,#5789);
#4836=LINE('',#56344,#5790);
#4837=LINE('',#56347,#5791);
#4838=LINE('',#56369,#5792);
#4839=LINE('',#56401,#5793);
#4840=LINE('',#56402,#5794);
#4841=LINE('',#56434,#5795);
#4842=LINE('',#56435,#5796);
#4843=LINE('',#56442,#5797);
#4844=LINE('',#56443,#5798);
#4845=LINE('',#56475,#5799);
#4846=LINE('',#56476,#5800);
#4847=LINE('',#56483,#5801);
#4848=LINE('',#56484,#5802);
#4849=LINE('',#56491,#5803);
#4850=LINE('',#56492,#5804);
#4851=LINE('',#56509,#5805);
#4852=LINE('',#56526,#5806);
#4853=LINE('',#56530,#5807);
#4854=LINE('',#56533,#5808);
#5786=VECTOR('',#22720,6.15985379710312);
#5787=VECTOR('',#22751,10.);
#5788=VECTOR('',#22754,10.);
#5789=VECTOR('',#22757,10.);
#5790=VECTOR('',#22760,10.);
#5791=VECTOR('',#22763,10.);
#5792=VECTOR('',#22766,10.);
#5793=VECTOR('',#22769,10.);
#5794=VECTOR('',#22770,10.);
#5795=VECTOR('',#22773,10.);
#5796=VECTOR('',#22774,10.);
#5797=VECTOR('',#22777,10.);
#5798=VECTOR('',#22778,10.);
#5799=VECTOR('',#22781,10.);
#5800=VECTOR('',#22782,10.);
#5801=VECTOR('',#22785,10.);
#5802=VECTOR('',#22786,10.);
#5803=VECTOR('',#22789,10.);
#5804=VECTOR('',#22790,10.);
#5805=VECTOR('',#22801,7.25527674973257);
#5806=VECTOR('',#22806,4.25);
#5807=VECTOR('',#22811,4.05);
#5808=VECTOR('',#22816,4.25);
#6672=B_SPLINE_CURVE_WITH_KNOTS('',3,(#55929,#55930,#55931,#55932,#55933,
#55934,#55935,#55936,#55937,#55938,#55939,#55940,#55941,#55942,#55943,#55944,
#55945,#55946,#55947),.UNSPECIFIED.,.F.,.F.,(4,3,3,3,3,3,4),(-0.136738994562975,
-0.122118862870872,-0.0885145718176996,-0.0747535058851621,-0.0395493225812212,
-0.00612228981501024,0.),.UNSPECIFIED.);
#6673=B_SPLINE_CURVE_WITH_KNOTS('',3,(#55951,#55952,#55953,#55954,#55955,
#55956,#55957,#55958,#55959,#55960,#55961,#55962,#55963,#55964,#55965,#55966,
#55967,#55968,#55969,#55970,#55971,#55972,#55973,#55974,#55975,#55976,#55977,
#55978,#55979,#55980,#55981),.UNSPECIFIED.,.F.,.F.,(4,3,3,3,3,3,3,3,3,3,
4),(-0.273459791663231,-0.23953153084867,-0.216807499006331,-0.179324588754136,
-0.164307407772797,-0.122118862870832,-0.0885145718176626,-0.0747535058851424,
-0.0395513512837351,-0.00612692919564764,0.),.UNSPECIFIED.);
#6674=B_SPLINE_CURVE_WITH_KNOTS('',3,(#55985,#55986,#55987,#55988,#55989,
#55990,#55991,#55992,#55993,#55994,#55995,#55996,#55997,#55998,#55999,#56000,
#56001,#56002,#56003,#56004,#56005,#56006,#56007,#56008,#56009,#56010,#56011,
#56012,#56013,#56014,#56015),.UNSPECIFIED.,.F.,.F.,(4,3,3,3,3,3,3,3,3,3,
4),(-0.273459791663253,-0.239669924355099,-0.21680749900636,-0.184963318451147,
-0.16430740777285,-0.122118862870878,-0.0827567027783513,-0.0747535058851617,
-0.0395111290131105,-0.00593748200146239,0.),.UNSPECIFIED.);
#6675=B_SPLINE_CURVE_WITH_KNOTS('',3,(#56019,#56020,#56021,#56022,#56023,
#56024,#56025,#56026,#56027,#56028,#56029,#56030,#56031,#56032,#56033,#56034,
#56035,#56036,#56037,#56038,#56039,#56040,#56041,#56042,#56043,#56044,#56045,
#56046,#56047,#56048,#56049),.UNSPECIFIED.,.F.,.F.,(4,3,3,3,3,3,3,3,3,3,
4),(-0.273459791663475,-0.239530723478153,-0.216807499006455,-0.179324881519317,
-0.164307407772862,-0.122118862870871,-0.0885145718177087,-0.0747535058851606,
-0.0395493225800805,-0.00612228981348414,0.),.UNSPECIFIED.);
#6676=B_SPLINE_CURVE_WITH_KNOTS('',3,(#56053,#56054,#56055,#56056,#56057,
#56058,#56059,#56060,#56061,#56062,#56063,#56064,#56065,#56066,#56067,#56068,
#56069,#56070,#56071,#56072,#56073,#56074,#56075,#56076,#56077,#56078,#56079,
#56080,#56081,#56082,#56083),.UNSPECIFIED.,.F.,.F.,(4,3,3,3,3,3,3,3,3,3,
4),(-0.273459791663443,-0.239531530848477,-0.216807499006449,-0.179324588753778,
-0.164307407772894,-0.122118862870893,-0.0885145718177228,-0.0747535058851679,
-0.0395513512850697,-0.00612692919683943,0.),.UNSPECIFIED.);
#6677=B_SPLINE_CURVE_WITH_KNOTS('',3,(#56087,#56088,#56089,#56090,#56091,
#56092,#56093,#56094,#56095,#56096,#56097,#56098,#56099,#56100,#56101,#56102,
#56103,#56104,#56105,#56106,#56107,#56108,#56109,#56110,#56111,#56112,#56113,
#56114,#56115,#56116,#56117),.UNSPECIFIED.,.F.,.F.,(4,3,3,3,3,3,3,3,3,3,
4),(-0.273459791663401,-0.239669924355128,-0.216807499006408,-0.184963318451192,
-0.164307407772861,-0.122118862870879,-0.0827567027776284,-0.0747535058851694,
-0.0395111290123009,-0.00593748200080557,0.),.UNSPECIFIED.);
#6678=B_SPLINE_CURVE_WITH_KNOTS('',3,(#56120,#56121,#56122,#56123,#56124,
#56125,#56126,#56127,#56128,#56129,#56130,#56131,#56132,#56133,#56134,#56135),
 .UNSPECIFIED.,.F.,.F.,(4,3,3,3,3,4),(-0.273459791663231,-0.239530723478429,
-0.216807499006338,-0.179324881517841,-0.16430740777284,-0.136738994562975),
 .UNSPECIFIED.);
#6679=B_SPLINE_CURVE_WITH_KNOTS('',3,(#56157,#56158,#56159,#56160),
 .UNSPECIFIED.,.F.,.F.,(4,4),(0.718335936055936,0.955209640017503),
 .UNSPECIFIED.);
#6680=B_SPLINE_CURVE_WITH_KNOTS('',3,(#56162,#56163,#56164,#56165,#56166,
#56167),.UNSPECIFIED.,.F.,.F.,(4,2,4),(-0.0458340621949542,-0.0229142437600697,
0.),.UNSPECIFIED.);
#6681=B_SPLINE_CURVE_WITH_KNOTS('',3,(#56169,#56170,#56171,#56172,#56173),
 .UNSPECIFIED.,.F.,.F.,(4,1,4),(-0.952706230317623,-0.504344050522728,-0.168698268101591),
 .UNSPECIFIED.);
#6682=B_SPLINE_CURVE_WITH_KNOTS('',3,(#56175,#56176,#56177,#56178,#56179,
#56180),.UNSPECIFIED.,.F.,.F.,(4,2,4),(-0.0458340597127026,-0.022919521896342,
0.),.UNSPECIFIED.);
#6683=B_SPLINE_CURVE_WITH_KNOTS('',3,(#56181,#56182,#56183,#56184),
 .UNSPECIFIED.,.F.,.F.,(4,4),(0.166194858401647,0.403068562363093),
 .UNSPECIFIED.);
#6684=B_SPLINE_CURVE_WITH_KNOTS('',3,(#56206,#56207,#56208,#56209),
 .UNSPECIFIED.,.F.,.F.,(4,4),(0.718335936055936,0.955209640017503),
 .UNSPECIFIED.);
#6685=B_SPLINE_CURVE_WITH_KNOTS('',3,(#56211,#56212,#56213,#56214,#56215,
#56216),.UNSPECIFIED.,.F.,.F.,(4,2,4),(-0.0458340621875639,-0.0229142437586445,
0.),.UNSPECIFIED.);
#6686=B_SPLINE_CURVE_WITH_KNOTS('',3,(#56218,#56219,#56220,#56221,#56222),
 .UNSPECIFIED.,.F.,.F.,(4,1,4),(-0.952706230317622,-0.504344050522728,-0.168698268101591),
 .UNSPECIFIED.);
#6687=B_SPLINE_CURVE_WITH_KNOTS('',3,(#56223,#56224,#56225,#56226,#56227,
#56228),.UNSPECIFIED.,.F.,.F.,(4,2,4),(-0.0458340597191651,-0.0229195218989816,
0.),.UNSPECIFIED.);
#6688=B_SPLINE_CURVE_WITH_KNOTS('',3,(#56229,#56230,#56231,#56232),
 .UNSPECIFIED.,.F.,.F.,(4,4),(0.166194858401647,0.403068562363093),
 .UNSPECIFIED.);
#6689=B_SPLINE_CURVE_WITH_KNOTS('',3,(#56235,#56236,#56237,#56238),
 .UNSPECIFIED.,.F.,.F.,(4,4),(0.166194858401646,0.403068562363093),
 .UNSPECIFIED.);
#6690=B_SPLINE_CURVE_WITH_KNOTS('',3,(#56241,#56242,#56243,#56244),
 .UNSPECIFIED.,.F.,.F.,(4,4),(0.166194858401646,0.403068562363093),
 .UNSPECIFIED.);
#6691=B_SPLINE_CURVE_WITH_KNOTS('',3,(#56245,#56246,#56247,#56248),
 .UNSPECIFIED.,.F.,.F.,(4,4),(0.718335936055935,0.955209640017502),
 .UNSPECIFIED.);
#6692=B_SPLINE_CURVE_WITH_KNOTS('',3,(#56251,#56252,#56253,#56254),
 .UNSPECIFIED.,.F.,.F.,(4,4),(0.166194858401647,0.403068562363092),
 .UNSPECIFIED.);
#6693=B_SPLINE_CURVE_WITH_KNOTS('',3,(#56255,#56256,#56257,#56258),
 .UNSPECIFIED.,.F.,.F.,(4,4),(0.718335936055935,0.955209640017502),
 .UNSPECIFIED.);
#6694=B_SPLINE_CURVE_WITH_KNOTS('',3,(#56261,#56262,#56263,#56264),
 .UNSPECIFIED.,.F.,.F.,(4,4),(0.166194858401647,0.403068562363094),
 .UNSPECIFIED.);
#6695=B_SPLINE_CURVE_WITH_KNOTS('',3,(#56265,#56266,#56267,#56268),
 .UNSPECIFIED.,.F.,.F.,(4,4),(0.718335936055935,0.955209640017502),
 .UNSPECIFIED.);
#6696=B_SPLINE_CURVE_WITH_KNOTS('',3,(#56270,#56271,#56272,#56273),
 .UNSPECIFIED.,.F.,.F.,(4,4),(0.718335936055935,0.955209640017502),
 .UNSPECIFIED.);
#6697=B_SPLINE_CURVE_WITH_KNOTS('',3,(#56295,#56296,#56297,#56298,#56299,
#56300),.UNSPECIFIED.,.F.,.F.,(4,2,4),(-0.0458340621934442,-0.0229142437595665,
0.),.UNSPECIFIED.);
#6698=B_SPLINE_CURVE_WITH_KNOTS('',3,(#56302,#56303,#56304,#56305,#56306),
 .UNSPECIFIED.,.F.,.F.,(4,1,4),(-0.952706230317622,-0.617060447896421,-0.168698268101591),
 .UNSPECIFIED.);
#6699=B_SPLINE_CURVE_WITH_KNOTS('',3,(#56307,#56308,#56309,#56310,#56311,
#56312),.UNSPECIFIED.,.F.,.F.,(4,2,4),(-0.0458340597159227,-0.022919521898133,
0.),.UNSPECIFIED.);
#6700=B_SPLINE_CURVE_WITH_KNOTS('',3,(#56320,#56321,#56322,#56323,#56324,
#56325),.UNSPECIFIED.,.F.,.F.,(4,2,4),(-0.045834059720736,-0.0229195218988986,
0.),.UNSPECIFIED.);
#6701=B_SPLINE_CURVE_WITH_KNOTS('',3,(#56331,#56332,#56333,#56334,#56335,
#56336),.UNSPECIFIED.,.F.,.F.,(4,2,4),(-0.0458340621946948,-0.0229142437601225,
0.),.UNSPECIFIED.);
#6702=B_SPLINE_CURVE_WITH_KNOTS('',3,(#56338,#56339,#56340,#56341,#56342,
#56343),.UNSPECIFIED.,.F.,.F.,(4,2,4),(-0.0458340597183968,-0.0229195218978244,
0.),.UNSPECIFIED.);
#6703=B_SPLINE_CURVE_WITH_KNOTS('',3,(#56348,#56349,#56350,#56351,#56352,
#56353),.UNSPECIFIED.,.F.,.F.,(4,2,4),(-0.0458340621954861,-0.0229142437603453,
0.),.UNSPECIFIED.);
#6704=B_SPLINE_CURVE_WITH_KNOTS('',3,(#56356,#56357,#56358,#56359,#56360,
#56361),.UNSPECIFIED.,.F.,.F.,(4,2,4),(-0.0458340621957891,-0.022914243760215,
0.),.UNSPECIFIED.);
#6705=B_SPLINE_CURVE_WITH_KNOTS('',3,(#56363,#56364,#56365,#56366,#56367,
#56368),.UNSPECIFIED.,.F.,.F.,(4,2,4),(-0.0458340597171303,-0.0229195218977166,
0.),.UNSPECIFIED.);
#6706=B_SPLINE_CURVE_WITH_KNOTS('',3,(#56390,#56391,#56392,#56393,#56394),
 .UNSPECIFIED.,.F.,.F.,(4,1,4),(-0.952706230317622,-0.617060447896421,-0.168698268101591),
 .UNSPECIFIED.);
#6707=B_SPLINE_CURVE_WITH_KNOTS('',3,(#56423,#56424,#56425,#56426,#56427),
 .UNSPECIFIED.,.F.,.F.,(4,1,4),(-0.952706230317622,-0.504344050522728,-0.168698268101591),
 .UNSPECIFIED.);
#6708=B_SPLINE_CURVE_WITH_KNOTS('',3,(#56464,#56465,#56466,#56467,#56468),
 .UNSPECIFIED.,.F.,.F.,(4,1,4),(-0.952706230317622,-0.504344050522728,-0.168698268101591),
 .UNSPECIFIED.);
#8239=VERTEX_POINT('',#55924);
#8240=VERTEX_POINT('',#55926);
#8241=VERTEX_POINT('',#55928);
#8242=VERTEX_POINT('',#55948);
#8243=VERTEX_POINT('',#55950);
#8244=VERTEX_POINT('',#55982);
#8245=VERTEX_POINT('',#55984);
#8246=VERTEX_POINT('',#56016);
#8247=VERTEX_POINT('',#56018);
#8248=VERTEX_POINT('',#56050);
#8249=VERTEX_POINT('',#56052);
#8250=VERTEX_POINT('',#56084);
#8251=VERTEX_POINT('',#56086);
#8252=VERTEX_POINT('',#56118);
#8253=VERTEX_POINT('',#56156);
#8254=VERTEX_POINT('',#56161);
#8255=VERTEX_POINT('',#56168);
#8256=VERTEX_POINT('',#56174);
#8257=VERTEX_POINT('',#56205);
#8258=VERTEX_POINT('',#56210);
#8259=VERTEX_POINT('',#56217);
#8260=VERTEX_POINT('',#56240);
#8261=VERTEX_POINT('',#56250);
#8262=VERTEX_POINT('',#56260);
#8263=VERTEX_POINT('',#56294);
#8264=VERTEX_POINT('',#56301);
#8265=VERTEX_POINT('',#56314);
#8266=VERTEX_POINT('',#56319);
#8267=VERTEX_POINT('',#56330);
#8268=VERTEX_POINT('',#56337);
#8269=VERTEX_POINT('',#56346);
#8270=VERTEX_POINT('',#56355);
#8271=VERTEX_POINT('',#56362);
#8272=VERTEX_POINT('',#56396);
#8273=VERTEX_POINT('',#56397);
#8274=VERTEX_POINT('',#56429);
#8275=VERTEX_POINT('',#56430);
#8276=VERTEX_POINT('',#56437);
#8277=VERTEX_POINT('',#56438);
#8278=VERTEX_POINT('',#56470);
#8279=VERTEX_POINT('',#56471);
#8280=VERTEX_POINT('',#56478);
#8281=VERTEX_POINT('',#56479);
#8282=VERTEX_POINT('',#56486);
#8283=VERTEX_POINT('',#56487);
#8284=VERTEX_POINT('',#56506);
#8285=VERTEX_POINT('',#56508);
#8286=VERTEX_POINT('',#56523);
#8287=VERTEX_POINT('',#56525);
#8288=VERTEX_POINT('',#56529);
#10679=EDGE_CURVE('',#8239,#8239,#1214,.T.);
#10680=EDGE_CURVE('',#8239,#8240,#4832,.T.);
#10681=EDGE_CURVE('',#8240,#8241,#6672,.T.);
#10682=EDGE_CURVE('',#8241,#8242,#1215,.T.);
#10683=EDGE_CURVE('',#8242,#8243,#6673,.T.);
#10684=EDGE_CURVE('',#8243,#8244,#1216,.T.);
#10685=EDGE_CURVE('',#8244,#8245,#6674,.T.);
#10686=EDGE_CURVE('',#8245,#8246,#1217,.T.);
#10687=EDGE_CURVE('',#8246,#8247,#6675,.T.);
#10688=EDGE_CURVE('',#8247,#8248,#1218,.T.);
#10689=EDGE_CURVE('',#8248,#8249,#6676,.T.);
#10690=EDGE_CURVE('',#8249,#8250,#1219,.T.);
#10691=EDGE_CURVE('',#8250,#8251,#6677,.T.);
#10692=EDGE_CURVE('',#8251,#8252,#1220,.T.);
#10693=EDGE_CURVE('',#8252,#8240,#6678,.T.);
#10694=EDGE_CURVE('',#8248,#8253,#6679,.T.);
#10695=EDGE_CURVE('',#8253,#8254,#6680,.F.);
#10696=EDGE_CURVE('',#8254,#8255,#6681,.T.);
#10697=EDGE_CURVE('',#8255,#8256,#6682,.F.);
#10698=EDGE_CURVE('',#8256,#8249,#6683,.T.);
#10699=EDGE_CURVE('',#8246,#8257,#6684,.T.);
#10700=EDGE_CURVE('',#8257,#8258,#6685,.F.);
#10701=EDGE_CURVE('',#8258,#8259,#6686,.T.);
#10702=EDGE_CURVE('',#8259,#8253,#6687,.F.);
#10703=EDGE_CURVE('',#8253,#8247,#6688,.T.);
#10704=EDGE_CURVE('',#8257,#8245,#6689,.T.);
#10705=EDGE_CURVE('',#8260,#8243,#6690,.T.);
#10706=EDGE_CURVE('',#8244,#8260,#6691,.T.);
#10707=EDGE_CURVE('',#8261,#8241,#6692,.T.);
#10708=EDGE_CURVE('',#8242,#8261,#6693,.T.);
#10709=EDGE_CURVE('',#8262,#8251,#6694,.T.);
#10710=EDGE_CURVE('',#8252,#8262,#6695,.T.);
#10711=EDGE_CURVE('',#8250,#8256,#6696,.T.);
#10712=EDGE_CURVE('',#8260,#8263,#6697,.F.);
#10713=EDGE_CURVE('',#8263,#8264,#6698,.T.);
#10714=EDGE_CURVE('',#8264,#8257,#6699,.F.);
#10715=EDGE_CURVE('',#8265,#8265,#1221,.T.);
#10716=EDGE_CURVE('',#8258,#8264,#4833,.T.);
#10717=EDGE_CURVE('',#8266,#8260,#6700,.F.);
#10718=EDGE_CURVE('',#8263,#8266,#4834,.T.);
#10719=EDGE_CURVE('',#8254,#8259,#4835,.T.);
#10720=EDGE_CURVE('',#8261,#8267,#6701,.F.);
#10721=EDGE_CURVE('',#8268,#8261,#6702,.F.);
#10722=EDGE_CURVE('',#8267,#8268,#4836,.T.);
#10723=EDGE_CURVE('',#8269,#8255,#4837,.T.);
#10724=EDGE_CURVE('',#8256,#8269,#6703,.F.);
#10725=EDGE_CURVE('',#8262,#8270,#6704,.F.);
#10726=EDGE_CURVE('',#8271,#8262,#6705,.F.);
#10727=EDGE_CURVE('',#8270,#8271,#4838,.T.);
#10728=EDGE_CURVE('',#8269,#8271,#6706,.T.);
#10729=EDGE_CURVE('',#8272,#8273,#1792,.T.);
#10730=EDGE_CURVE('',#8273,#8270,#4839,.T.);
#10731=EDGE_CURVE('',#8271,#8272,#4840,.T.);
#10732=EDGE_CURVE('',#8270,#8268,#6707,.T.);
#10733=EDGE_CURVE('',#8274,#8275,#1793,.T.);
#10734=EDGE_CURVE('',#8275,#8269,#4841,.T.);
#10735=EDGE_CURVE('',#8255,#8274,#4842,.T.);
#10736=EDGE_CURVE('',#8276,#8277,#1794,.T.);
#10737=EDGE_CURVE('',#8277,#8267,#4843,.T.);
#10738=EDGE_CURVE('',#8268,#8276,#4844,.T.);
#10739=EDGE_CURVE('',#8267,#8266,#6708,.T.);
#10740=EDGE_CURVE('',#8278,#8279,#1795,.T.);
#10741=EDGE_CURVE('',#8279,#8254,#4845,.T.);
#10742=EDGE_CURVE('',#8259,#8278,#4846,.T.);
#10743=EDGE_CURVE('',#8280,#8281,#1796,.T.);
#10744=EDGE_CURVE('',#8281,#8263,#4847,.T.);
#10745=EDGE_CURVE('',#8266,#8280,#4848,.T.);
#10746=EDGE_CURVE('',#8282,#8283,#1797,.T.);
#10747=EDGE_CURVE('',#8283,#8258,#4849,.T.);
#10748=EDGE_CURVE('',#8264,#8282,#4850,.T.);
#10749=EDGE_CURVE('',#8279,#8274,#1798,.T.);
#10750=EDGE_CURVE('',#8283,#8278,#1799,.T.);
#10751=EDGE_CURVE('',#8281,#8282,#1800,.T.);
#10752=EDGE_CURVE('',#8284,#8284,#1222,.T.);
#10753=EDGE_CURVE('',#8284,#8285,#4851,.T.);
#10754=EDGE_CURVE('',#8273,#8285,#1801,.T.);
#10755=EDGE_CURVE('',#8275,#8272,#1802,.T.);
#10756=EDGE_CURVE('',#8277,#8280,#1803,.T.);
#10757=EDGE_CURVE('',#8285,#8276,#1804,.T.);
#10758=EDGE_CURVE('',#8286,#8286,#1223,.T.);
#10759=EDGE_CURVE('',#8286,#8287,#4852,.T.);
#10760=EDGE_CURVE('',#8287,#8287,#1224,.T.);
#10761=EDGE_CURVE('',#8287,#8288,#4853,.T.);
#10762=EDGE_CURVE('',#8288,#8288,#1225,.T.);
#10763=EDGE_CURVE('',#8288,#8265,#4854,.T.);
#15544=ORIENTED_EDGE('',*,*,#10679,.T.);
#15545=ORIENTED_EDGE('',*,*,#10680,.T.);
#15546=ORIENTED_EDGE('',*,*,#10681,.T.);
#15547=ORIENTED_EDGE('',*,*,#10682,.T.);
#15548=ORIENTED_EDGE('',*,*,#10683,.T.);
#15549=ORIENTED_EDGE('',*,*,#10684,.T.);
#15550=ORIENTED_EDGE('',*,*,#10685,.T.);
#15551=ORIENTED_EDGE('',*,*,#10686,.T.);
#15552=ORIENTED_EDGE('',*,*,#10687,.T.);
#15553=ORIENTED_EDGE('',*,*,#10688,.T.);
#15554=ORIENTED_EDGE('',*,*,#10689,.T.);
#15555=ORIENTED_EDGE('',*,*,#10690,.T.);
#15556=ORIENTED_EDGE('',*,*,#10691,.T.);
#15557=ORIENTED_EDGE('',*,*,#10692,.T.);
#15558=ORIENTED_EDGE('',*,*,#10693,.T.);
#15559=ORIENTED_EDGE('',*,*,#10680,.F.);
#15560=ORIENTED_EDGE('',*,*,#10689,.F.);
#15561=ORIENTED_EDGE('',*,*,#10694,.T.);
#15562=ORIENTED_EDGE('',*,*,#10695,.T.);
#15563=ORIENTED_EDGE('',*,*,#10696,.T.);
#15564=ORIENTED_EDGE('',*,*,#10697,.T.);
#15565=ORIENTED_EDGE('',*,*,#10698,.T.);
#15566=ORIENTED_EDGE('',*,*,#10687,.F.);
#15567=ORIENTED_EDGE('',*,*,#10699,.T.);
#15568=ORIENTED_EDGE('',*,*,#10700,.T.);
#15569=ORIENTED_EDGE('',*,*,#10701,.T.);
#15570=ORIENTED_EDGE('',*,*,#10702,.T.);
#15571=ORIENTED_EDGE('',*,*,#10703,.T.);
#15572=ORIENTED_EDGE('',*,*,#10688,.F.);
#15573=ORIENTED_EDGE('',*,*,#10703,.F.);
#15574=ORIENTED_EDGE('',*,*,#10694,.F.);
#15575=ORIENTED_EDGE('',*,*,#10686,.F.);
#15576=ORIENTED_EDGE('',*,*,#10704,.F.);
#15577=ORIENTED_EDGE('',*,*,#10699,.F.);
#15578=ORIENTED_EDGE('',*,*,#10684,.F.);
#15579=ORIENTED_EDGE('',*,*,#10705,.F.);
#15580=ORIENTED_EDGE('',*,*,#10706,.F.);
#15581=ORIENTED_EDGE('',*,*,#10682,.F.);
#15582=ORIENTED_EDGE('',*,*,#10707,.F.);
#15583=ORIENTED_EDGE('',*,*,#10708,.F.);
#15584=ORIENTED_EDGE('',*,*,#10692,.F.);
#15585=ORIENTED_EDGE('',*,*,#10709,.F.);
#15586=ORIENTED_EDGE('',*,*,#10710,.F.);
#15587=ORIENTED_EDGE('',*,*,#10690,.F.);
#15588=ORIENTED_EDGE('',*,*,#10698,.F.);
#15589=ORIENTED_EDGE('',*,*,#10711,.F.);
#15590=ORIENTED_EDGE('',*,*,#10685,.F.);
#15591=ORIENTED_EDGE('',*,*,#10706,.T.);
#15592=ORIENTED_EDGE('',*,*,#10712,.T.);
#15593=ORIENTED_EDGE('',*,*,#10713,.T.);
#15594=ORIENTED_EDGE('',*,*,#10714,.T.);
#15595=ORIENTED_EDGE('',*,*,#10704,.T.);
#15596=ORIENTED_EDGE('',*,*,#10679,.F.);
#15597=ORIENTED_EDGE('',*,*,#10715,.T.);
#15598=ORIENTED_EDGE('',*,*,#10716,.F.);
#15599=ORIENTED_EDGE('',*,*,#10700,.F.);
#15600=ORIENTED_EDGE('',*,*,#10714,.F.);
#15601=ORIENTED_EDGE('',*,*,#10712,.F.);
#15602=ORIENTED_EDGE('',*,*,#10717,.F.);
#15603=ORIENTED_EDGE('',*,*,#10718,.F.);
#15604=ORIENTED_EDGE('',*,*,#10719,.F.);
#15605=ORIENTED_EDGE('',*,*,#10695,.F.);
#15606=ORIENTED_EDGE('',*,*,#10702,.F.);
#15607=ORIENTED_EDGE('',*,*,#10720,.F.);
#15608=ORIENTED_EDGE('',*,*,#10721,.F.);
#15609=ORIENTED_EDGE('',*,*,#10722,.F.);
#15610=ORIENTED_EDGE('',*,*,#10723,.F.);
#15611=ORIENTED_EDGE('',*,*,#10724,.F.);
#15612=ORIENTED_EDGE('',*,*,#10697,.F.);
#15613=ORIENTED_EDGE('',*,*,#10725,.F.);
#15614=ORIENTED_EDGE('',*,*,#10726,.F.);
#15615=ORIENTED_EDGE('',*,*,#10727,.F.);
#15616=ORIENTED_EDGE('',*,*,#10691,.F.);
#15617=ORIENTED_EDGE('',*,*,#10711,.T.);
#15618=ORIENTED_EDGE('',*,*,#10724,.T.);
#15619=ORIENTED_EDGE('',*,*,#10728,.T.);
#15620=ORIENTED_EDGE('',*,*,#10726,.T.);
#15621=ORIENTED_EDGE('',*,*,#10709,.T.);
#15622=ORIENTED_EDGE('',*,*,#10729,.T.);
#15623=ORIENTED_EDGE('',*,*,#10730,.T.);
#15624=ORIENTED_EDGE('',*,*,#10727,.T.);
#15625=ORIENTED_EDGE('',*,*,#10731,.T.);
#15626=ORIENTED_EDGE('',*,*,#10693,.F.);
#15627=ORIENTED_EDGE('',*,*,#10710,.T.);
#15628=ORIENTED_EDGE('',*,*,#10725,.T.);
#15629=ORIENTED_EDGE('',*,*,#10732,.T.);
#15630=ORIENTED_EDGE('',*,*,#10721,.T.);
#15631=ORIENTED_EDGE('',*,*,#10707,.T.);
#15632=ORIENTED_EDGE('',*,*,#10681,.F.);
#15633=ORIENTED_EDGE('',*,*,#10733,.T.);
#15634=ORIENTED_EDGE('',*,*,#10734,.T.);
#15635=ORIENTED_EDGE('',*,*,#10723,.T.);
#15636=ORIENTED_EDGE('',*,*,#10735,.T.);
#15637=ORIENTED_EDGE('',*,*,#10736,.T.);
#15638=ORIENTED_EDGE('',*,*,#10737,.T.);
#15639=ORIENTED_EDGE('',*,*,#10722,.T.);
#15640=ORIENTED_EDGE('',*,*,#10738,.T.);
#15641=ORIENTED_EDGE('',*,*,#10683,.F.);
#15642=ORIENTED_EDGE('',*,*,#10708,.T.);
#15643=ORIENTED_EDGE('',*,*,#10720,.T.);
#15644=ORIENTED_EDGE('',*,*,#10739,.T.);
#15645=ORIENTED_EDGE('',*,*,#10717,.T.);
#15646=ORIENTED_EDGE('',*,*,#10705,.T.);
#15647=ORIENTED_EDGE('',*,*,#10740,.T.);
#15648=ORIENTED_EDGE('',*,*,#10741,.T.);
#15649=ORIENTED_EDGE('',*,*,#10719,.T.);
#15650=ORIENTED_EDGE('',*,*,#10742,.T.);
#15651=ORIENTED_EDGE('',*,*,#10743,.T.);
#15652=ORIENTED_EDGE('',*,*,#10744,.T.);
#15653=ORIENTED_EDGE('',*,*,#10718,.T.);
#15654=ORIENTED_EDGE('',*,*,#10745,.T.);
#15655=ORIENTED_EDGE('',*,*,#10746,.T.);
#15656=ORIENTED_EDGE('',*,*,#10747,.T.);
#15657=ORIENTED_EDGE('',*,*,#10716,.T.);
#15658=ORIENTED_EDGE('',*,*,#10748,.T.);
#15659=ORIENTED_EDGE('',*,*,#10735,.F.);
#15660=ORIENTED_EDGE('',*,*,#10696,.F.);
#15661=ORIENTED_EDGE('',*,*,#10741,.F.);
#15662=ORIENTED_EDGE('',*,*,#10749,.T.);
#15663=ORIENTED_EDGE('',*,*,#10742,.F.);
#15664=ORIENTED_EDGE('',*,*,#10701,.F.);
#15665=ORIENTED_EDGE('',*,*,#10747,.F.);
#15666=ORIENTED_EDGE('',*,*,#10750,.T.);
#15667=ORIENTED_EDGE('',*,*,#10748,.F.);
#15668=ORIENTED_EDGE('',*,*,#10713,.F.);
#15669=ORIENTED_EDGE('',*,*,#10744,.F.);
#15670=ORIENTED_EDGE('',*,*,#10751,.T.);
#15671=ORIENTED_EDGE('',*,*,#10752,.F.);
#15672=ORIENTED_EDGE('',*,*,#10753,.T.);
#15673=ORIENTED_EDGE('',*,*,#10754,.F.);
#15674=ORIENTED_EDGE('',*,*,#10729,.F.);
#15675=ORIENTED_EDGE('',*,*,#10755,.F.);
#15676=ORIENTED_EDGE('',*,*,#10733,.F.);
#15677=ORIENTED_EDGE('',*,*,#10749,.F.);
#15678=ORIENTED_EDGE('',*,*,#10740,.F.);
#15679=ORIENTED_EDGE('',*,*,#10750,.F.);
#15680=ORIENTED_EDGE('',*,*,#10746,.F.);
#15681=ORIENTED_EDGE('',*,*,#10751,.F.);
#15682=ORIENTED_EDGE('',*,*,#10743,.F.);
#15683=ORIENTED_EDGE('',*,*,#10756,.F.);
#15684=ORIENTED_EDGE('',*,*,#10736,.F.);
#15685=ORIENTED_EDGE('',*,*,#10757,.F.);
#15686=ORIENTED_EDGE('',*,*,#10753,.F.);
#15687=ORIENTED_EDGE('',*,*,#10758,.F.);
#15688=ORIENTED_EDGE('',*,*,#10759,.T.);
#15689=ORIENTED_EDGE('',*,*,#10760,.T.);
#15690=ORIENTED_EDGE('',*,*,#10759,.F.);
#15691=ORIENTED_EDGE('',*,*,#10760,.F.);
#15692=ORIENTED_EDGE('',*,*,#10761,.T.);
#15693=ORIENTED_EDGE('',*,*,#10762,.T.);
#15694=ORIENTED_EDGE('',*,*,#10761,.F.);
#15695=ORIENTED_EDGE('',*,*,#10762,.F.);
#15696=ORIENTED_EDGE('',*,*,#10763,.T.);
#15697=ORIENTED_EDGE('',*,*,#10715,.F.);
#15698=ORIENTED_EDGE('',*,*,#10763,.F.);
#15699=ORIENTED_EDGE('',*,*,#10737,.F.);
#15700=ORIENTED_EDGE('',*,*,#10756,.T.);
#15701=ORIENTED_EDGE('',*,*,#10745,.F.);
#15702=ORIENTED_EDGE('',*,*,#10739,.F.);
#15703=ORIENTED_EDGE('',*,*,#10730,.F.);
#15704=ORIENTED_EDGE('',*,*,#10754,.T.);
#15705=ORIENTED_EDGE('',*,*,#10757,.T.);
#15706=ORIENTED_EDGE('',*,*,#10738,.F.);
#15707=ORIENTED_EDGE('',*,*,#10732,.F.);
#15708=ORIENTED_EDGE('',*,*,#10734,.F.);
#15709=ORIENTED_EDGE('',*,*,#10755,.T.);
#15710=ORIENTED_EDGE('',*,*,#10731,.F.);
#15711=ORIENTED_EDGE('',*,*,#10728,.F.);
#15712=ORIENTED_EDGE('',*,*,#10752,.T.);
#15713=ORIENTED_EDGE('',*,*,#10758,.T.);
#15956=PLANE('',#18702);
#15957=PLANE('',#18704);
#15958=PLANE('',#18705);
#15959=PLANE('',#18706);
#15960=PLANE('',#18707);
#15961=PLANE('',#18708);
#15962=PLANE('',#18709);
#15963=PLANE('',#18710);
#15964=PLANE('',#18711);
#15965=PLANE('',#18712);
#15966=PLANE('',#18713);
#15967=PLANE('',#18714);
#15968=PLANE('',#18715);
#15969=PLANE('',#18716);
#15970=PLANE('',#18717);
#15971=PLANE('',#18718);
#15972=PLANE('',#18727);
#15973=PLANE('',#18728);
#15974=PLANE('',#18729);
#15975=PLANE('',#18730);
#16912=ADVANCED_FACE('',(#2741),#652,.T.);
#16913=ADVANCED_FACE('',(#2742),#361,.T.);
#16914=ADVANCED_FACE('',(#2743),#362,.T.);
#16915=ADVANCED_FACE('',(#2744),#653,.T.);
#16916=ADVANCED_FACE('',(#2745),#654,.T.);
#16917=ADVANCED_FACE('',(#2746),#655,.T.);
#16918=ADVANCED_FACE('',(#2747),#656,.T.);
#16919=ADVANCED_FACE('',(#2748),#657,.T.);
#16920=ADVANCED_FACE('',(#2749),#658,.T.);
#16921=ADVANCED_FACE('',(#2750),#363,.T.);
#16922=ADVANCED_FACE('',(#2751,#562),#15956,.T.);
#16923=ADVANCED_FACE('',(#2752),#15957,.T.);
#16924=ADVANCED_FACE('',(#2753),#15958,.T.);
#16925=ADVANCED_FACE('',(#2754),#15959,.T.);
#16926=ADVANCED_FACE('',(#2755),#15960,.T.);
#16927=ADVANCED_FACE('',(#2756),#15961,.T.);
#16928=ADVANCED_FACE('',(#2757),#15962,.T.);
#16929=ADVANCED_FACE('',(#2758),#364,.T.);
#16930=ADVANCED_FACE('',(#2759),#15963,.T.);
#16931=ADVANCED_FACE('',(#2760),#365,.T.);
#16932=ADVANCED_FACE('',(#2761),#15964,.T.);
#16933=ADVANCED_FACE('',(#2762),#15965,.T.);
#16934=ADVANCED_FACE('',(#2763),#366,.T.);
#16935=ADVANCED_FACE('',(#2764),#15966,.T.);
#16936=ADVANCED_FACE('',(#2765),#15967,.T.);
#16937=ADVANCED_FACE('',(#2766),#15968,.T.);
#16938=ADVANCED_FACE('',(#2767),#15969,.T.);
#16939=ADVANCED_FACE('',(#2768),#15970,.T.);
#16940=ADVANCED_FACE('',(#2769),#15971,.T.);
#16941=ADVANCED_FACE('',(#2770),#659,.T.);
#16942=ADVANCED_FACE('',(#2771),#660,.F.);
#16943=ADVANCED_FACE('',(#2772),#1760,.F.);
#16944=ADVANCED_FACE('',(#2773),#661,.F.);
#16945=ADVANCED_FACE('',(#2774),#15972,.T.);
#16946=ADVANCED_FACE('',(#2775),#15973,.T.);
#16947=ADVANCED_FACE('',(#2776),#15974,.T.);
#16948=ADVANCED_FACE('',(#2777,#563),#15975,.F.);
#16968=CLOSED_SHELL('',(#16912,#16913,#16914,#16915,#16916,#16917,#16918,
#16919,#16920,#16921,#16922,#16923,#16924,#16925,#16926,#16927,#16928,#16929,
#16930,#16931,#16932,#16933,#16934,#16935,#16936,#16937,#16938,#16939,#16940,
#16941,#16942,#16943,#16944,#16945,#16946,#16947,#16948));
#18687=AXIS2_PLACEMENT_3D('',#55922,#22714,#22715);
#18688=AXIS2_PLACEMENT_3D('',#55923,#22716,#22717);
#18689=AXIS2_PLACEMENT_3D('',#55925,#22718,#22719);
#18690=AXIS2_PLACEMENT_3D('',#55949,#22721,#22722);
#18691=AXIS2_PLACEMENT_3D('',#55983,#22723,#22724);
#18692=AXIS2_PLACEMENT_3D('',#56017,#22725,#22726);
#18693=AXIS2_PLACEMENT_3D('',#56051,#22727,#22728);
#18694=AXIS2_PLACEMENT_3D('',#56085,#22729,#22730);
#18695=AXIS2_PLACEMENT_3D('',#56119,#22731,#22732);
#18696=AXIS2_PLACEMENT_3D('',#56233,#22733,#22734);
#18697=AXIS2_PLACEMENT_3D('',#56234,#22735,#22736);
#18698=AXIS2_PLACEMENT_3D('',#56239,#22737,#22738);
#18699=AXIS2_PLACEMENT_3D('',#56249,#22739,#22740);
#18700=AXIS2_PLACEMENT_3D('',#56259,#22741,#22742);
#18701=AXIS2_PLACEMENT_3D('',#56269,#22743,#22744);
#18702=AXIS2_PLACEMENT_3D('',#56313,#22745,#22746);
#18703=AXIS2_PLACEMENT_3D('',#56315,#22747,#22748);
#18704=AXIS2_PLACEMENT_3D('',#56316,#22749,#22750);
#18705=AXIS2_PLACEMENT_3D('',#56318,#22752,#22753);
#18706=AXIS2_PLACEMENT_3D('',#56327,#22755,#22756);
#18707=AXIS2_PLACEMENT_3D('',#56329,#22758,#22759);
#18708=AXIS2_PLACEMENT_3D('',#56345,#22761,#22762);
#18709=AXIS2_PLACEMENT_3D('',#56354,#22764,#22765);
#18710=AXIS2_PLACEMENT_3D('',#56395,#22767,#22768);
#18711=AXIS2_PLACEMENT_3D('',#56428,#22771,#22772);
#18712=AXIS2_PLACEMENT_3D('',#56436,#22775,#22776);
#18713=AXIS2_PLACEMENT_3D('',#56469,#22779,#22780);
#18714=AXIS2_PLACEMENT_3D('',#56477,#22783,#22784);
#18715=AXIS2_PLACEMENT_3D('',#56485,#22787,#22788);
#18716=AXIS2_PLACEMENT_3D('',#56493,#22791,#22792);
#18717=AXIS2_PLACEMENT_3D('',#56497,#22793,#22794);
#18718=AXIS2_PLACEMENT_3D('',#56501,#22795,#22796);
#18719=AXIS2_PLACEMENT_3D('',#56505,#22797,#22798);
#18720=AXIS2_PLACEMENT_3D('',#56507,#22799,#22800);
#18721=AXIS2_PLACEMENT_3D('',#56522,#22802,#22803);
#18722=AXIS2_PLACEMENT_3D('',#56524,#22804,#22805);
#18723=AXIS2_PLACEMENT_3D('',#56527,#22807,#22808);
#18724=AXIS2_PLACEMENT_3D('',#56528,#22809,#22810);
#18725=AXIS2_PLACEMENT_3D('',#56531,#22812,#22813);
#18726=AXIS2_PLACEMENT_3D('',#56532,#22814,#22815);
#18727=AXIS2_PLACEMENT_3D('',#56534,#22817,#22818);
#18728=AXIS2_PLACEMENT_3D('',#56535,#22819,#22820);
#18729=AXIS2_PLACEMENT_3D('',#56536,#22821,#22822);
#18730=AXIS2_PLACEMENT_3D('',#56537,#22823,#22824);
#22714=DIRECTION('axis',(0.,0.,1.));
#22715=DIRECTION('refdir',(1.,0.,0.));
#22716=DIRECTION('center_axis',(-1.,0.,-2.9053353178063E-15));
#22717=DIRECTION('ref_axis',(0.,1.,3.18680589015166E-17));
#22718=DIRECTION('center_axis',(-1.,0.,0.));
#22719=DIRECTION('ref_axis',(0.,1.,0.));
#22720=DIRECTION('',(-0.259092713651731,-0.965852455467491,-9.01813866303348E-16));
#22721=DIRECTION('center_axis',(1.,0.,0.));
#22722=DIRECTION('ref_axis',(0.,1.,6.12323399573677E-17));
#22723=DIRECTION('center_axis',(1.,0.,0.));
#22724=DIRECTION('ref_axis',(0.,1.,6.12323399573677E-17));
#22725=DIRECTION('center_axis',(1.,0.,0.));
#22726=DIRECTION('ref_axis',(0.,1.,6.12323399573677E-17));
#22727=DIRECTION('center_axis',(1.,0.,0.));
#22728=DIRECTION('ref_axis',(0.,1.,6.12323399573677E-17));
#22729=DIRECTION('center_axis',(1.,0.,0.));
#22730=DIRECTION('ref_axis',(0.,1.,6.12323399573677E-17));
#22731=DIRECTION('center_axis',(1.,0.,0.));
#22732=DIRECTION('ref_axis',(0.,1.,6.12323399573677E-17));
#22733=DIRECTION('center_axis',(-1.,0.,0.));
#22734=DIRECTION('ref_axis',(0.,1.,0.));
#22735=DIRECTION('center_axis',(-1.,0.,0.));
#22736=DIRECTION('ref_axis',(0.,1.,0.));
#22737=DIRECTION('center_axis',(-1.,0.,0.));
#22738=DIRECTION('ref_axis',(0.,1.,0.));
#22739=DIRECTION('center_axis',(-1.,0.,0.));
#22740=DIRECTION('ref_axis',(0.,1.,0.));
#22741=DIRECTION('center_axis',(-1.,0.,0.));
#22742=DIRECTION('ref_axis',(0.,1.,0.));
#22743=DIRECTION('center_axis',(-1.,0.,0.));
#22744=DIRECTION('ref_axis',(0.,1.,0.));
#22745=DIRECTION('center_axis',(1.,0.,0.));
#22746=DIRECTION('ref_axis',(0.,0.,-1.));
#22747=DIRECTION('center_axis',(-1.,0.,0.));
#22748=DIRECTION('ref_axis',(0.,1.,0.));
#22749=DIRECTION('center_axis',(0.369302787980288,0.804805310675672,-0.46465456276488));
#22750=DIRECTION('ref_axis',(-0.78285445475425,0.,-0.622204871944464));
#22751=DIRECTION('',(-1.04457232346762E-13,-0.499999999999998,-0.86602540378444));
#22752=DIRECTION('center_axis',(0.369302787980293,-9.03801697827166E-13,
-0.929309125528197));
#22753=DIRECTION('ref_axis',(-0.929309125528197,0.,-0.369302787980293));
#22754=DIRECTION('',(-1.06831260354642E-13,-1.,0.));
#22755=DIRECTION('center_axis',(0.369302787980294,0.804805310676573,0.464654562763313));
#22756=DIRECTION('ref_axis',(0.782854454753223,0.,-0.622204871945755));
#22757=DIRECTION('',(-1.06831260354642E-13,0.500000000000001,-0.866025403784438));
#22758=DIRECTION('center_axis',(0.369302787980299,-0.804805310676573,-0.464654562763311));
#22759=DIRECTION('ref_axis',(-0.782854454753218,0.,-0.622204871945762));
#22760=DIRECTION('',(-9.73351483231188E-14,-0.499999999999998,0.86602540378444));
#22761=DIRECTION('center_axis',(0.369302787980296,9.02065506036524E-13,
0.929309125528196));
#22762=DIRECTION('ref_axis',(0.929309125528196,0.,-0.369302787980296));
#22763=DIRECTION('',(-1.02083204338881E-13,1.,0.));
#22764=DIRECTION('center_axis',(0.369302787980293,-0.804805310675669,0.464654562764882));
#22765=DIRECTION('ref_axis',(0.782854454754247,0.,-0.622204871944466));
#22766=DIRECTION('',(-1.04457232346761E-13,0.500000000000001,0.866025403784438));
#22767=DIRECTION('center_axis',(0.,-0.866025403784438,0.500000000000001));
#22768=DIRECTION('ref_axis',(1.,0.,0.));
#22769=DIRECTION('',(1.,0.,0.));
#22770=DIRECTION('',(-1.,0.,0.));
#22771=DIRECTION('center_axis',(0.,0.,1.));
#22772=DIRECTION('ref_axis',(1.,0.,0.));
#22773=DIRECTION('',(1.,0.,0.));
#22774=DIRECTION('',(-1.,0.,0.));
#22775=DIRECTION('center_axis',(0.,-0.86602540378444,-0.499999999999998));
#22776=DIRECTION('ref_axis',(0.,0.499999999999998,-0.86602540378444));
#22777=DIRECTION('',(1.,0.,0.));
#22778=DIRECTION('',(-1.,0.,0.));
#22779=DIRECTION('center_axis',(0.,0.866025403784438,0.500000000000001));
#22780=DIRECTION('ref_axis',(1.,0.,0.));
#22781=DIRECTION('',(1.,0.,0.));
#22782=DIRECTION('',(-1.,0.,0.));
#22783=DIRECTION('center_axis',(0.,0.,-1.));
#22784=DIRECTION('ref_axis',(-1.,0.,0.));
#22785=DIRECTION('',(1.,0.,0.));
#22786=DIRECTION('',(-1.,0.,0.));
#22787=DIRECTION('center_axis',(0.,0.86602540378444,-0.499999999999998));
#22788=DIRECTION('ref_axis',(0.,0.499999999999998,0.86602540378444));
#22789=DIRECTION('',(1.,0.,0.));
#22790=DIRECTION('',(-1.,0.,0.));
#22791=DIRECTION('center_axis',(0.,0.5,0.866025403784439));
#22792=DIRECTION('ref_axis',(0.,-0.866025403784439,0.5));
#22793=DIRECTION('center_axis',(0.,1.,-4.43760619934668E-16));
#22794=DIRECTION('ref_axis',(0.,4.43760619934668E-16,1.));
#22795=DIRECTION('center_axis',(0.,0.5,-0.866025403784439));
#22796=DIRECTION('ref_axis',(0.,0.866025403784439,0.5));
#22797=DIRECTION('center_axis',(1.,0.,0.));
#22798=DIRECTION('ref_axis',(0.,1.,0.));
#22799=DIRECTION('center_axis',(-1.,0.,0.));
#22800=DIRECTION('ref_axis',(0.,1.,0.));
#22801=DIRECTION('',(0.500490667348524,-0.865741931465162,-1.06022808525646E-16));
#22802=DIRECTION('center_axis',(-1.,0.,0.));
#22803=DIRECTION('ref_axis',(0.,1.,0.));
#22804=DIRECTION('center_axis',(1.,0.,0.));
#22805=DIRECTION('ref_axis',(0.,1.,0.));
#22806=DIRECTION('',(0.78086880944303,0.624695047554425,7.6503079043073E-17));
#22807=DIRECTION('center_axis',(1.,0.,0.));
#22808=DIRECTION('ref_axis',(0.,0.,-1.));
#22809=DIRECTION('center_axis',(1.,0.,0.));
#22810=DIRECTION('ref_axis',(0.,1.,0.));
#22811=DIRECTION('',(1.,0.,0.));
#22812=DIRECTION('center_axis',(1.,0.,0.));
#22813=DIRECTION('ref_axis',(0.,0.,-1.));
#22814=DIRECTION('center_axis',(1.,0.,0.));
#22815=DIRECTION('ref_axis',(0.,1.,0.));
#22816=DIRECTION('',(0.78086880944303,-0.624695047554424,-7.65030790430729E-17));
#22817=DIRECTION('center_axis',(0.,-0.5,-0.866025403784439));
#22818=DIRECTION('ref_axis',(0.,0.866025403784439,-0.5));
#22819=DIRECTION('center_axis',(0.,-1.,-1.4792020664489E-16));
#22820=DIRECTION('ref_axis',(0.,1.4792020664489E-16,-1.));
#22821=DIRECTION('center_axis',(0.,-0.5,0.866025403784439));
#22822=DIRECTION('ref_axis',(0.,-0.866025403784439,-0.5));
#22823=DIRECTION('center_axis',(1.,0.,0.));
#22824=DIRECTION('ref_axis',(0.,0.,-1.));
#55922=CARTESIAN_POINT('',(0.,0.,0.));
#55923=CARTESIAN_POINT('Origin',(6.73243375990795,0.,-1.96302583630813E-16));
#55924=CARTESIAN_POINT('',(6.8,-5.90797863635533,7.23518712644349E-16));
#55925=CARTESIAN_POINT('Origin',(6.8,0.,0.));
#55926=CARTESIAN_POINT('',(6.69652890400909,-6.29699688036588,-0.000745309284438215));
#55927=CARTESIAN_POINT('',(6.73243375990795,-6.15985379710312,-1.14696969084543E-15));
#55928=CARTESIAN_POINT('',(6.66502947251616,-6.26458164591552,-1.36312261022737));
#55929=CARTESIAN_POINT('Ctrl Pts',(6.69652890400909,-6.29699688036588,-0.000745309284438218));
#55930=CARTESIAN_POINT('Ctrl Pts',(6.69636098644092,-6.29700262112883,-0.0492132156999537));
#55931=CARTESIAN_POINT('Ctrl Pts',(6.69608278371896,-6.29688319686096,-0.0976832249692937));
#55932=CARTESIAN_POINT('Ctrl Pts',(6.69569933387107,-6.29663841314834,-0.146165083532695));
#55933=CARTESIAN_POINT('Ctrl Pts',(6.69481798076397,-6.29607578185022,-0.257599830262322));
#55934=CARTESIAN_POINT('Ctrl Pts',(6.69338166738899,-6.29485127594458,-0.368971942752256));
#55935=CARTESIAN_POINT('Ctrl Pts',(6.69145929669846,-6.29296756829865,-0.480391711796666));
#55936=CARTESIAN_POINT('Ctrl Pts',(6.69067207967973,-6.2921961839218,-0.526018467783933));
#55937=CARTESIAN_POINT('Ctrl Pts',(6.68980345947523,-6.29131421828673,-0.571653020364473));
#55938=CARTESIAN_POINT('Ctrl Pts',(6.68884893267613,-6.29032205090899,-0.61730213483034));
#55939=CARTESIAN_POINT('Ctrl Pts',(6.68640701890517,-6.28778384330171,-0.734083770874912));
#55940=CARTESIAN_POINT('Ctrl Pts',(6.68340625854999,-6.284527919109,-0.850780859498688));
#55941=CARTESIAN_POINT('Ctrl Pts',(6.67978096417448,-6.28057025686126,-0.967522815650963));
#55942=CARTESIAN_POINT('Ctrl Pts',(6.67633867912469,-6.27681238227884,-1.07837149405382));
#55943=CARTESIAN_POINT('Ctrl Pts',(6.6723331936121,-6.27242175564932,-1.18926081995884));
#55944=CARTESIAN_POINT('Ctrl Pts',(6.66772997716308,-6.26741032190845,-1.30025872695154));
#55945=CARTESIAN_POINT('Ctrl Pts',(6.66688688033845,-6.26649245851432,-1.32058842119099));
#55946=CARTESIAN_POINT('Ctrl Pts',(6.66602379657714,-6.26555376669622,-1.34092163259341));
#55947=CARTESIAN_POINT('Ctrl Pts',(6.66514060252649,-6.26459431597002,-1.36125860576499));
#55948=CARTESIAN_POINT('',(6.66836161846084,-4.31130259409624,-4.74443759007071));
#55949=CARTESIAN_POINT('Origin',(6.6648675198159,0.,-3.92605167261626E-16));
#55950=CARTESIAN_POINT('',(6.66503408817778,-1.95314743508685,-6.10607994622927));
#55951=CARTESIAN_POINT('Ctrl Pts',(6.66935871145732,-4.31020955205977,-4.74503293761719));
#55952=CARTESIAN_POINT('Ctrl Pts',(6.67436042918073,-4.21520368992507,-4.80602391498316));
#55953=CARTESIAN_POINT('Ctrl Pts',(6.67866531126362,-4.11997191868513,-4.86641425169366));
#55954=CARTESIAN_POINT('Ctrl Pts',(6.68227076873634,-4.02444968243747,-4.92622621540924));
#55955=CARTESIAN_POINT('Ctrl Pts',(6.68468558542453,-3.96047203412808,-4.96628629910921));
#55956=CARTESIAN_POINT('Ctrl Pts',(6.68678714553132,-3.89636312663956,-5.00608746781467));
#55957=CARTESIAN_POINT('Ctrl Pts',(6.68858007739062,-3.83209320725026,-5.04564199838796));
#55958=CARTESIAN_POINT('Ctrl Pts',(6.69153748848899,-3.72608105073249,-5.11088653464953));
#55959=CARTESIAN_POINT('Ctrl Pts',(6.69364912704048,-3.61978338152845,-5.17536640559943));
#55960=CARTESIAN_POINT('Ctrl Pts',(6.69495610000005,-3.51307967515119,-5.23914030618921));
#55961=CARTESIAN_POINT('Ctrl Pts',(6.69547972661654,-3.47032982303817,-5.26469072905122));
#55962=CARTESIAN_POINT('Ctrl Pts',(6.69587456241581,-3.42751433350044,-5.29012805821525));
#55963=CARTESIAN_POINT('Ctrl Pts',(6.69614463629548,-3.38462385382883,-5.3154568011996));
#55964=CARTESIAN_POINT('Ctrl Pts',(6.69690336884412,-3.26412940618645,-5.38661415170591));
#55965=CARTESIAN_POINT('Ctrl Pts',(6.69667276210013,-3.14322205465598,-5.45680979375134));
#55966=CARTESIAN_POINT('Ctrl Pts',(6.69556561628492,-3.02171103015008,-5.52614860785243));
#55967=CARTESIAN_POINT('Ctrl Pts',(6.69468374538135,-2.92492428760768,-5.58137880590142));
#55968=CARTESIAN_POINT('Ctrl Pts',(6.69324805633593,-2.82786106051647,-5.63600435237614));
#55969=CARTESIAN_POINT('Ctrl Pts',(6.69132764292846,-2.73042720868452,-5.69008268017868));
#55970=CARTESIAN_POINT('Ctrl Pts',(6.69054122742349,-2.69052773105539,-5.71222793041573));
#55971=CARTESIAN_POINT('Ctrl Pts',(6.68967363179484,-2.65056625226925,-5.73428128569138));
#55972=CARTESIAN_POINT('Ctrl Pts',(6.6887203269053,-2.61053709848336,-5.75624646027473));
#55973=CARTESIAN_POINT('Ctrl Pts',(6.68628167961823,-2.50813860209913,-5.81243552842698));
#55974=CARTESIAN_POINT('Ctrl Pts',(6.68328553552123,-2.40545474077465,-5.86796068128634));
#55975=CARTESIAN_POINT('Ctrl Pts',(6.6796657811188,-2.30238136543676,-5.92290049980573));
#55976=CARTESIAN_POINT('Ctrl Pts',(6.67622882675131,-2.20451326496543,-5.97506582049214));
#55977=CARTESIAN_POINT('Ctrl Pts',(6.67222952719711,-2.10629379186944,-6.02670346636737));
#55978=CARTESIAN_POINT('Ctrl Pts',(6.66763300366906,-2.0076700314861,-6.07785777969868));
#55979=CARTESIAN_POINT('Ctrl Pts',(6.66679042891553,-1.98959160980734,-6.0872347213555));
#55980=CARTESIAN_POINT('Ctrl Pts',(6.6659278508756,-1.9714997104692,-6.09659535683047));
#55981=CARTESIAN_POINT('Ctrl Pts',(6.66504514382671,-1.95339415559984,-6.10593986928562));
#55982=CARTESIAN_POINT('',(6.66503408817778,1.95314743508651,-6.10607994622938));
#55983=CARTESIAN_POINT('Origin',(6.6648675198159,0.,-3.92605167261626E-16));
#55984=CARTESIAN_POINT('',(6.6683616184638,4.31130259409795,-4.74443759006966));
#55985=CARTESIAN_POINT('Ctrl Pts',(6.66504514382671,1.95339415559952,-6.10593986928573));
#55986=CARTESIAN_POINT('Ctrl Pts',(6.66991331462735,2.05324714040973,-6.05440444455141));
#55987=CARTESIAN_POINT('Ctrl Pts',(6.67416697695882,2.15269731478132,-6.00237315124276));
#55988=CARTESIAN_POINT('Ctrl Pts',(6.67783901815979,2.25179789322377,-5.94979970935148));
#55989=CARTESIAN_POINT('Ctrl Pts',(6.68032354309352,2.3188499344761,-5.91422820563398));
#55990=CARTESIAN_POINT('Ctrl Pts',(6.68254235212595,2.38574287168437,-5.87840794797414));
#55991=CARTESIAN_POINT('Ctrl Pts',(6.68451150443652,2.45250341609415,-5.84231823937542));
#55992=CARTESIAN_POINT('Ctrl Pts',(6.68725425988621,2.54549157451221,-5.79205029189074));
#55993=CARTESIAN_POINT('Ctrl Pts',(6.68950868260796,2.63811000348344,-5.74132073890011));
#55994=CARTESIAN_POINT('Ctrl Pts',(6.6913278663153,2.730427135972,-5.69008257296905));
#55995=CARTESIAN_POINT('Ctrl Pts',(6.69250789027921,2.79030917437,-5.65684664224831));
#55996=CARTESIAN_POINT('Ctrl Pts',(6.69350522572667,2.85006491766445,-5.62339639406913));
#55997=CARTESIAN_POINT('Ctrl Pts',(6.69430363820578,2.90971680597308,-5.58971757209521));
#55998=CARTESIAN_POINT('Ctrl Pts',(6.69593435114067,3.03155245909875,-5.52093045758735));
#55999=CARTESIAN_POINT('Ctrl Pts',(6.69672978737442,3.15277519167217,-5.45129218342463));
#56000=CARTESIAN_POINT('Ctrl Pts',(6.69656720749179,3.27357451204812,-5.38069560740119));
#56001=CARTESIAN_POINT('Ctrl Pts',(6.69641551950675,3.38628098720044,-5.31482858748203));
#56002=CARTESIAN_POINT('Ctrl Pts',(6.69543013844524,3.49847401422254,-5.24821175049788));
#56003=CARTESIAN_POINT('Ctrl Pts',(6.69353943304081,3.61030941318271,-5.18076617701774));
#56004=CARTESIAN_POINT('Ctrl Pts',(6.69315501085506,3.63304802090655,-5.16705300165168));
#56005=CARTESIAN_POINT('Ctrl Pts',(6.69273328275894,3.65577173256785,-5.1533056124498));
#56006=CARTESIAN_POINT('Ctrl Pts',(6.6922738380125,3.67848166516312,-5.13952343023613));
#56007=CARTESIAN_POINT('Ctrl Pts',(6.6902506558864,3.77848570279241,-5.07883307534723));
#56008=CARTESIAN_POINT('Ctrl Pts',(6.68749862281492,3.87806838929537,-5.01756113610782));
#56009=CARTESIAN_POINT('Ctrl Pts',(6.68399280879373,3.97734644961371,-4.95565755544302));
#56010=CARTESIAN_POINT('Ctrl Pts',(6.68065299539626,4.07192368443615,-4.89668511514642));
#56011=CARTESIAN_POINT('Ctrl Pts',(6.67662905286536,4.16622462203365,-4.83713926971924));
#56012=CARTESIAN_POINT('Ctrl Pts',(6.6719206958442,4.26031186570891,-4.77699710220824));
#56013=CARTESIAN_POINT('Ctrl Pts',(6.67108802535535,4.27695114578758,-4.76636099118337));
#56014=CARTESIAN_POINT('Ctrl Pts',(6.67023400615726,4.29358363828582,-4.75570628669163));
#56015=CARTESIAN_POINT('Ctrl Pts',(6.66935871145733,4.31020955205948,-4.74503293761744));
#56016=CARTESIAN_POINT('',(6.66844118715618,6.2644530578692,-1.36147101261479));
#56017=CARTESIAN_POINT('Origin',(6.6648675198159,0.,-3.92605167261626E-16));
#56018=CARTESIAN_POINT('',(6.66512518996691,6.26459255876718,1.3615171235111));
#56019=CARTESIAN_POINT('Ctrl Pts',(6.66943768476099,6.26442235049373,-1.36025300281069));
#56020=CARTESIAN_POINT('Ctrl Pts',(6.67444551486767,6.26973920227163,-1.24747868336829));
#56021=CARTESIAN_POINT('Ctrl Pts',(6.67875641270276,6.27442290417064,-1.13480902487606));
#56022=CARTESIAN_POINT('Ctrl Pts',(6.682367556141,6.27846046253376,-1.02217693285355));
#56023=CARTESIAN_POINT('Ctrl Pts',(6.68478603761825,6.28116452574297,-0.94674414183892));
#56024=CARTESIAN_POINT('Ctrl Pts',(6.68689115132044,6.28357875541318,-0.871327101016574));
#56025=CARTESIAN_POINT('Ctrl Pts',(6.68868745028096,6.28569890792413,-0.795893893215038));
#56026=CARTESIAN_POINT('Ctrl Pts',(6.69165049748906,6.28919616095181,-0.67146463022138));
#56027=CARTESIAN_POINT('Ctrl Pts',(6.6937672098887,6.29188845823143,-0.547170307559333));
#56028=CARTESIAN_POINT('Ctrl Pts',(6.69507834981273,6.2937663704627,-0.422877132573859));
#56029=CARTESIAN_POINT('Ctrl Pts',(6.69560366022879,6.29451875915703,-0.373078862939984));
#56030=CARTESIAN_POINT('Ctrl Pts',(6.69600002716747,6.29514038349348,-0.323280264512499));
#56031=CARTESIAN_POINT('Ctrl Pts',(6.6962714577742,6.29563047084122,-0.273470978596723));
#56032=CARTESIAN_POINT('Ctrl Pts',(6.69703398698074,6.29700727178824,-0.133541897922291));
#56033=CARTESIAN_POINT('Ctrl Pts',(6.69680582961814,6.29734476924276,0.00626420573700309));
#56034=CARTESIAN_POINT('Ctrl Pts',(6.69569933387107,6.29663841314834,0.146165083532808));
#56035=CARTESIAN_POINT('Ctrl Pts',(6.69481798076397,6.29607578185022,0.257599830262394));
#56036=CARTESIAN_POINT('Ctrl Pts',(6.69338166738899,6.29485127594458,0.368971942752287));
#56037=CARTESIAN_POINT('Ctrl Pts',(6.69145929669845,6.29296756829865,0.480391711796661));
#56038=CARTESIAN_POINT('Ctrl Pts',(6.69067207967973,6.2921961839218,0.526018467783964));
#56039=CARTESIAN_POINT('Ctrl Pts',(6.68980345947522,6.29131421828673,0.57165302036454));
#56040=CARTESIAN_POINT('Ctrl Pts',(6.68884893267613,6.29032205090899,0.617302134830443));
#56041=CARTESIAN_POINT('Ctrl Pts',(6.68640701890508,6.28778384330163,0.734083770878798));
#56042=CARTESIAN_POINT('Ctrl Pts',(6.68340625854979,6.28452791910879,0.850780859506348));
#56043=CARTESIAN_POINT('Ctrl Pts',(6.67978096417412,6.28057025686087,0.967522815662406));
#56044=CARTESIAN_POINT('Ctrl Pts',(6.67633867912425,6.27681238227837,1.07837149406654));
#56045=CARTESIAN_POINT('Ctrl Pts',(6.67233319361156,6.27242175564875,1.18926081997286));
#56046=CARTESIAN_POINT('Ctrl Pts',(6.66772997716244,6.26741032190776,1.30025872696685));
#56047=CARTESIAN_POINT('Ctrl Pts',(6.66688688033801,6.26649245851385,1.32058842120122));
#56048=CARTESIAN_POINT('Ctrl Pts',(6.66602379657691,6.26555376669599,1.34092163259858));
#56049=CARTESIAN_POINT('Ctrl Pts',(6.66514060252648,6.26459431597002,1.36125860576509));
#56050=CARTESIAN_POINT('',(6.66836161846091,4.3113025940965,4.74443759007056));
#56051=CARTESIAN_POINT('Origin',(6.6648675198159,0.,-3.92605167261626E-16));
#56052=CARTESIAN_POINT('',(6.66503408817681,1.95314743508669,6.10607994622942));
#56053=CARTESIAN_POINT('Ctrl Pts',(6.66935871145727,4.31020955206015,4.74503293761698));
#56054=CARTESIAN_POINT('Ctrl Pts',(6.67436042918074,4.21520368992431,4.80602391498368));
#56055=CARTESIAN_POINT('Ctrl Pts',(6.67866531126367,4.11997191868325,4.86641425169488));
#56056=CARTESIAN_POINT('Ctrl Pts',(6.68227076873642,4.02444968243447,4.92622621541114));
#56057=CARTESIAN_POINT('Ctrl Pts',(6.68468558542457,3.96047203412598,4.96628629911054));
#56058=CARTESIAN_POINT('Ctrl Pts',(6.68678714553132,3.89636312663836,5.00608746781543));
#56059=CARTESIAN_POINT('Ctrl Pts',(6.68858007739059,3.83209320724997,5.04564199838816));
#56060=CARTESIAN_POINT('Ctrl Pts',(6.691537488489,3.72608105073089,5.11088653465053));
#56061=CARTESIAN_POINT('Ctrl Pts',(6.6936491270405,3.61978338152556,5.17536640560121));
#56062=CARTESIAN_POINT('Ctrl Pts',(6.69495610000006,3.51307967514701,5.23914030619173));
#56063=CARTESIAN_POINT('Ctrl Pts',(6.69547972661653,3.47032982303531,5.26469072905295));
#56064=CARTESIAN_POINT('Ctrl Pts',(6.69587456241578,3.4275143334989,5.29012805821618));
#56065=CARTESIAN_POINT('Ctrl Pts',(6.69614463629545,3.38462385382863,5.31545680119975));
#56066=CARTESIAN_POINT('Ctrl Pts',(6.69690336884408,3.26412940618622,5.38661415170606));
#56067=CARTESIAN_POINT('Ctrl Pts',(6.69667276210009,3.14322205465577,5.45680979375149));
#56068=CARTESIAN_POINT('Ctrl Pts',(6.69556561628488,3.02171103014988,5.52614860785257));
#56069=CARTESIAN_POINT('Ctrl Pts',(6.69468374538131,2.92492428760756,5.58137880590151));
#56070=CARTESIAN_POINT('Ctrl Pts',(6.69324805633589,2.82786106051644,5.63600435237619));
#56071=CARTESIAN_POINT('Ctrl Pts',(6.69132764292842,2.73042720868454,5.6900826801787));
#56072=CARTESIAN_POINT('Ctrl Pts',(6.69054122742345,2.69052773105532,5.71222793041579));
#56073=CARTESIAN_POINT('Ctrl Pts',(6.68967363179479,2.65056625226909,5.73428128569149));
#56074=CARTESIAN_POINT('Ctrl Pts',(6.68872032690526,2.61053709848311,5.7562464602749));
#56075=CARTESIAN_POINT('Ctrl Pts',(6.68628167961827,2.50813860210269,5.81243552842505));
#56076=CARTESIAN_POINT('Ctrl Pts',(6.68328553552141,2.40545474078205,5.86796068128236));
#56077=CARTESIAN_POINT('Ctrl Pts',(6.67966578111915,2.30238136544803,5.92290049979975));
#56078=CARTESIAN_POINT('Ctrl Pts',(6.6762288267517,2.20451326497631,5.97506582048642));
#56079=CARTESIAN_POINT('Ctrl Pts',(6.67222952719752,2.10629379187994,6.0267034663619));
#56080=CARTESIAN_POINT('Ctrl Pts',(6.66763300366949,2.0076700314962,6.07785777969347));
#56081=CARTESIAN_POINT('Ctrl Pts',(6.66679042891581,1.98959160981393,6.08723472135212));
#56082=CARTESIAN_POINT('Ctrl Pts',(6.66592785087571,1.97149971047227,6.09659535682891));
#56083=CARTESIAN_POINT('Ctrl Pts',(6.66504514382665,1.95339415559939,6.10593986928588));
#56084=CARTESIAN_POINT('',(6.66503408817771,-1.95314743508628,6.10607994622951));
#56085=CARTESIAN_POINT('Origin',(6.6648675198159,0.,-3.92605167261626E-16));
#56086=CARTESIAN_POINT('',(6.66836161846092,-4.31130259409623,4.7444375900708));
#56087=CARTESIAN_POINT('Ctrl Pts',(6.66504514382665,-1.95339415559905,6.105939869286));
#56088=CARTESIAN_POINT('Ctrl Pts',(6.6699133146273,-2.05324714040958,6.05440444455152));
#56089=CARTESIAN_POINT('Ctrl Pts',(6.67416697695878,-2.15269731478148,6.00237315124271));
#56090=CARTESIAN_POINT('Ctrl Pts',(6.67783901815976,-2.25179789322423,5.94979970935126));
#56091=CARTESIAN_POINT('Ctrl Pts',(6.6803235430935,-2.31884993447649,5.9142282056338));
#56092=CARTESIAN_POINT('Ctrl Pts',(6.68254235212591,-2.38574287168466,5.87840794797402));
#56093=CARTESIAN_POINT('Ctrl Pts',(6.68451150443648,-2.45250341609436,5.84231823937534));
#56094=CARTESIAN_POINT('Ctrl Pts',(6.68725425988618,-2.54549157451238,5.79205029189068));
#56095=CARTESIAN_POINT('Ctrl Pts',(6.68950868260793,-2.63811000348354,5.74132073890009));
#56096=CARTESIAN_POINT('Ctrl Pts',(6.69132786631526,-2.73042713597201,5.69008257296907));
#56097=CARTESIAN_POINT('Ctrl Pts',(6.69250789027917,-2.79030917437005,5.65684664224831));
#56098=CARTESIAN_POINT('Ctrl Pts',(6.69350522572663,-2.85006491766454,5.62339639406911));
#56099=CARTESIAN_POINT('Ctrl Pts',(6.69430363820574,-2.9097168059732,5.58971757209517));
#56100=CARTESIAN_POINT('Ctrl Pts',(6.69593435114063,-3.03155245909877,5.52093045758737));
#56101=CARTESIAN_POINT('Ctrl Pts',(6.69672978737438,-3.15277519167224,5.45129218342462));
#56102=CARTESIAN_POINT('Ctrl Pts',(6.69656720749175,-3.27357451204824,5.38069560740115));
#56103=CARTESIAN_POINT('Ctrl Pts',(6.69641551950671,-3.38628098720265,5.31482858748076));
#56104=CARTESIAN_POINT('Ctrl Pts',(6.69543013844517,-3.49847401422682,5.24821175049536));
#56105=CARTESIAN_POINT('Ctrl Pts',(6.69353943304067,-3.61030941318907,5.18076617701393));
#56106=CARTESIAN_POINT('Ctrl Pts',(6.69315501085495,-3.63304802091084,5.16705300164911));
#56107=CARTESIAN_POINT('Ctrl Pts',(6.69273328275886,-3.65577173257007,5.15330561244848));
#56108=CARTESIAN_POINT('Ctrl Pts',(6.69227383801246,-3.67848166516327,5.13952343023606));
#56109=CARTESIAN_POINT('Ctrl Pts',(6.69025065588632,-3.77848570279493,5.07883307534573));
#56110=CARTESIAN_POINT('Ctrl Pts',(6.68749862281475,-3.87806838930023,5.01756113610486));
#56111=CARTESIAN_POINT('Ctrl Pts',(6.68399280879344,-3.97734644962088,4.95565755543857));
#56112=CARTESIAN_POINT('Ctrl Pts',(6.68065299539596,-4.07192368444291,4.89668511514219));
#56113=CARTESIAN_POINT('Ctrl Pts',(6.67662905286504,-4.16622462203999,4.83713926971524));
#56114=CARTESIAN_POINT('Ctrl Pts',(6.67192069584387,-4.26031186571482,4.77699710220449));
#56115=CARTESIAN_POINT('Ctrl Pts',(6.67108802535511,-4.27695114579165,4.76636099118079));
#56116=CARTESIAN_POINT('Ctrl Pts',(6.67023400615712,-4.29358363828805,4.75570628669022));
#56117=CARTESIAN_POINT('Ctrl Pts',(6.66935871145727,-4.31020955205987,4.74503293761721));
#56118=CARTESIAN_POINT('',(6.6684411871562,-6.2644530578692,1.36147101261486));
#56119=CARTESIAN_POINT('Origin',(6.6648675198159,0.,-3.92605167261626E-16));
#56120=CARTESIAN_POINT('Ctrl Pts',(6.66943768476097,-6.26442235049373,1.36025300281079));
#56121=CARTESIAN_POINT('Ctrl Pts',(6.67444551486759,-6.26973920227156,1.2474786833699));
#56122=CARTESIAN_POINT('Ctrl Pts',(6.67875641270264,-6.27442290417052,1.13480902487915));
#56123=CARTESIAN_POINT('Ctrl Pts',(6.68236755614085,-6.2784604625336,1.02217693285811));
#56124=CARTESIAN_POINT('Ctrl Pts',(6.68478603761816,-6.28116452574288,0.946744141841997));
#56125=CARTESIAN_POINT('Ctrl Pts',(6.68689115132039,-6.28357875541314,0.871327101018171));
#56126=CARTESIAN_POINT('Ctrl Pts',(6.68868745028095,-6.28569890792413,0.79589389321515));
#56127=CARTESIAN_POINT('Ctrl Pts',(6.69165049748917,-6.28919616095194,0.671464630216681));
#56128=CARTESIAN_POINT('Ctrl Pts',(6.69376720988886,-6.29188845823163,0.547170307549914));
#56129=CARTESIAN_POINT('Ctrl Pts',(6.69507834981288,-6.29376637046291,0.422877132559733));
#56130=CARTESIAN_POINT('Ctrl Pts',(6.69560366022886,-6.29451875915715,0.373078862930602));
#56131=CARTESIAN_POINT('Ctrl Pts',(6.69600002716749,-6.29514038349353,0.323280264507863));
#56132=CARTESIAN_POINT('Ctrl Pts',(6.6962714577742,-6.29563047084122,0.273470978596836));
#56133=CARTESIAN_POINT('Ctrl Pts',(6.69676973994398,-6.29653015488919,0.182032951914047));
#56134=CARTESIAN_POINT('Ctrl Pts',(6.69684570354175,-6.29698595925452,0.0906480036726336));
#56135=CARTESIAN_POINT('Ctrl Pts',(6.69652890400909,-6.29699688036588,-0.000745309284438218));
#56136=CARTESIAN_POINT('Ctrl Pts',(5.82127992530897,0.211713211864508,7.38332081960416));
#56137=CARTESIAN_POINT('Ctrl Pts',(6.14241820370575,1.20871426115459,6.80770199541419));
#56138=CARTESIAN_POINT('Ctrl Pts',(6.49215447047434,3.14708040407219,5.68858578101266));
#56139=CARTESIAN_POINT('Ctrl Pts',(6.2494642965047,4.95895205574989,4.64250119517949));
#56140=CARTESIAN_POINT('Ctrl Pts',(5.82127992530902,6.28828678813546,3.87500942959356));
#56141=CARTESIAN_POINT('Ctrl Pts',(5.94576262842914,0.141142141243011,7.33053715581116));
#56142=CARTESIAN_POINT('Ctrl Pts',(6.27212071493947,1.14515484589772,6.75259524852742));
#56143=CARTESIAN_POINT('Ctrl Pts',(6.63166480681812,3.1065235293192,5.62357322350997));
#56144=CARTESIAN_POINT('Ctrl Pts',(6.38090674377616,4.94116869510222,4.56154066351441));
#56145=CARTESIAN_POINT('Ctrl Pts',(5.94576262842917,6.27786032969667,3.78750125776656));
#56146=CARTESIAN_POINT('Ctrl Pts',(6.07024533154931,0.0705710706215141,
7.27775349201815));
#56147=CARTESIAN_POINT('Ctrl Pts',(6.40182322617319,1.08159543064085,6.69748850164065));
#56148=CARTESIAN_POINT('Ctrl Pts',(6.7711751431619,3.06596665456621,5.55856066600728));
#56149=CARTESIAN_POINT('Ctrl Pts',(6.51234919104763,4.92338533445454,4.48058013184934));
#56150=CARTESIAN_POINT('Ctrl Pts',(6.07024533154933,6.26743387125788,3.69999308593956));
#56151=CARTESIAN_POINT('Ctrl Pts',(6.19472803466948,1.72084568816899E-14,
7.22496982822515));
#56152=CARTESIAN_POINT('Ctrl Pts',(6.53152573740691,1.01803601538398,6.64238175475387));
#56153=CARTESIAN_POINT('Ctrl Pts',(6.91068547950568,3.02540977981322,5.49354810850458));
#56154=CARTESIAN_POINT('Ctrl Pts',(6.64379163831909,4.90560197380687,4.39961960018427));
#56155=CARTESIAN_POINT('Ctrl Pts',(6.19472803466948,6.25700741281908,3.61248491411256));
#56156=CARTESIAN_POINT('',(6.19472803466948,6.25700741281908,3.61248491411256));
#56157=CARTESIAN_POINT('Ctrl Pts',(6.66935871145421,4.31020955208199,4.7450329376043));
#56158=CARTESIAN_POINT('Ctrl Pts',(6.58472768457026,4.91347707050904,4.39484321142667));
#56159=CARTESIAN_POINT('Ctrl Pts',(6.43065501953876,5.54701219617073,4.02602614003615));
#56160=CARTESIAN_POINT('Ctrl Pts',(6.19472803466948,6.25700741281908,3.61248491411256));
#56161=CARTESIAN_POINT('',(5.82838302289405,6.26617314097884,3.8877767497322));
#56162=CARTESIAN_POINT('Ctrl Pts',(5.82838302289405,6.26617314097884,3.8877767497322));
#56163=CARTESIAN_POINT('Ctrl Pts',(5.88949356894947,6.26458780816846,3.84195257738004));
#56164=CARTESIAN_POINT('Ctrl Pts',(5.95058218580133,6.26303119380756,3.7960960923254));
#56165=CARTESIAN_POINT('Ctrl Pts',(6.07269657345126,6.25997595306932,3.70433263349585));
#56166=CARTESIAN_POINT('Ctrl Pts',(6.13372433579515,6.25847726314342,3.65842418692963));
#56167=CARTESIAN_POINT('Ctrl Pts',(6.19472803466948,6.25700741281908,3.61248491411256));
#56168=CARTESIAN_POINT('',(5.82838302289383,0.233826859021799,7.37055349946514));
#56169=CARTESIAN_POINT('Ctrl Pts',(5.82838558568782,6.26617071740664,3.88777814898226));
#56170=CARTESIAN_POINT('Ctrl Pts',(6.25099836192328,4.94745326120368,4.6491400273061));
#56171=CARTESIAN_POINT('Ctrl Pts',(6.49028076601058,3.14668033196789,5.68881676274977));
#56172=CARTESIAN_POINT('Ctrl Pts',(6.14463154721472,1.22101319991002,6.800601199813));
#56173=CARTESIAN_POINT('Ctrl Pts',(5.82838421256034,0.233829133738886,7.37055218615661));
#56174=CARTESIAN_POINT('',(6.19472803466948,1.64850575197389E-14,7.22496982822515));
#56175=CARTESIAN_POINT('Ctrl Pts',(6.19472803466948,1.80893230908424E-14,
7.22496982822515));
#56176=CARTESIAN_POINT('Ctrl Pts',(6.13372354963894,0.0390501553628601,
7.24921270476878));
#56177=CARTESIAN_POINT('Ctrl Pts',(6.07269500050579,0.078059193557057,7.27346514426615));
#56178=CARTESIAN_POINT('Ctrl Pts',(5.95058061166719,0.156001057525407,7.32199279024714));
#56179=CARTESIAN_POINT('Ctrl Pts',(5.88949278160536,0.194935129147796,7.34626878768841));
#56180=CARTESIAN_POINT('Ctrl Pts',(5.82838302289431,0.233826859022126,7.37055349946495));
#56181=CARTESIAN_POINT('Ctrl Pts',(6.19472803466948,1.72084568816899E-14,
7.22496982822515));
#56182=CARTESIAN_POINT('Ctrl Pts',(6.4306550195388,0.71313481548644,6.81686654700397));
#56183=CARTESIAN_POINT('Ctrl Pts',(6.58105248112949,1.34886989409368,6.45303961304062));
#56184=CARTESIAN_POINT('Ctrl Pts',(6.66504514382361,1.95339415557755,6.10593986929842));
#56185=CARTESIAN_POINT('Ctrl Pts',(5.82127992530897,6.5,3.50831139001062));
#56186=CARTESIAN_POINT('Ctrl Pts',(6.14241820370575,6.5,2.35707374163067));
#56187=CARTESIAN_POINT('Ctrl Pts',(6.49243586254982,6.5,0.118785051139947));
#56188=CARTESIAN_POINT('Ctrl Pts',(6.2494642965047,6.5,-1.97332785883874));
#56189=CARTESIAN_POINT('Ctrl Pts',(5.82127992530902,6.5,-3.50831139001059));
#56190=CARTESIAN_POINT('Ctrl Pts',(5.94576262842914,6.4190024709397,3.5430358980446));
#56191=CARTESIAN_POINT('Ctrl Pts',(6.27212071493947,6.4204964496477,2.38456443644942));
#56192=CARTESIAN_POINT('Ctrl Pts',(6.63194145333222,6.42341735463559,0.121399944768468));
#56193=CARTESIAN_POINT('Ctrl Pts',(6.38090674377616,6.42099444255031,-1.99840728258573));
#56194=CARTESIAN_POINT('Ctrl Pts',(5.94576262842917,6.41900247093969,-3.54303589804459));
#56195=CARTESIAN_POINT('Ctrl Pts',(6.07024533154931,6.33800494187939,3.57776040607858));
#56196=CARTESIAN_POINT('Ctrl Pts',(6.40182322617319,6.3409928992954,2.41205513126817));
#56197=CARTESIAN_POINT('Ctrl Pts',(6.77144704411462,6.34683470927118,0.124014838396988));
#56198=CARTESIAN_POINT('Ctrl Pts',(6.51234919104763,6.34198888510063,-2.02348670633271));
#56199=CARTESIAN_POINT('Ctrl Pts',(6.07024533154933,6.33800494187938,-3.5777604060786));
#56200=CARTESIAN_POINT('Ctrl Pts',(6.19472803466948,6.25700741281908,3.61248491411256));
#56201=CARTESIAN_POINT('Ctrl Pts',(6.53152573740691,6.2614893489431,2.43954582608692));
#56202=CARTESIAN_POINT('Ctrl Pts',(6.91095263489701,6.27025206390677,0.12662973202551));
#56203=CARTESIAN_POINT('Ctrl Pts',(6.64379163831909,6.26298332765094,-2.0485661300797));
#56204=CARTESIAN_POINT('Ctrl Pts',(6.19472803466948,6.25700741281906,-3.6124849141126));
#56205=CARTESIAN_POINT('',(6.19472803466948,6.25700741281907,-3.61248491411259));
#56206=CARTESIAN_POINT('Ctrl Pts',(6.66943768475789,6.26442235049367,-1.36025300283622));
#56207=CARTESIAN_POINT('Ctrl Pts',(6.58476982174516,6.2627836062947,-2.05778423124321));
#56208=CARTESIAN_POINT('Ctrl Pts',(6.43065501953876,6.26014701165687,-2.79084040696789));
#56209=CARTESIAN_POINT('Ctrl Pts',(6.19472803466948,6.25700741281906,-3.6124849141126));
#56210=CARTESIAN_POINT('',(5.82838302289405,6.5,-3.4827767497333));
#56211=CARTESIAN_POINT('Ctrl Pts',(5.82838302289405,6.5,-3.4827767497333));
#56212=CARTESIAN_POINT('Ctrl Pts',(5.88949356895823,6.45952243622465,-3.50431589742522));
#56213=CARTESIAN_POINT('Ctrl Pts',(5.9505821858056,6.41903124806158,-3.52589607237054));
#56214=CARTESIAN_POINT('Ctrl Pts',(6.07269657345908,6.33803414120459,-3.56913188569258));
#56215=CARTESIAN_POINT('Ctrl Pts',(6.13372433579894,6.29752691526968,-3.59078820542605));
#56216=CARTESIAN_POINT('Ctrl Pts',(6.19472803466948,6.25700741281906,-3.6124849141126));
#56217=CARTESIAN_POINT('',(5.82838302289382,6.5,3.48277674973257));
#56218=CARTESIAN_POINT('Ctrl Pts',(5.82838560050068,6.5,-3.48277395419486));
#56219=CARTESIAN_POINT('Ctrl Pts',(6.25100014187621,6.5,-1.96005055047028));
#56220=CARTESIAN_POINT('Ctrl Pts',(6.49056037813313,6.5,0.119247370498949));
#56221=CARTESIAN_POINT('Ctrl Pts',(6.14463332716764,6.5,2.34287179454352));
#56222=CARTESIAN_POINT('Ctrl Pts',(5.82838423229859,6.5,3.48277411916905));
#56223=CARTESIAN_POINT('Ctrl Pts',(6.19472803466948,6.25700741281908,3.61248491411256));
#56224=CARTESIAN_POINT('Ctrl Pts',(6.13372354963881,6.29752743744818,3.59078792581838));
#56225=CARTESIAN_POINT('Ctrl Pts',(6.07269500050538,6.33803518525394,3.56913132751359));
#56226=CARTESIAN_POINT('Ctrl Pts',(5.95058061167076,6.41903229144087,3.52589551629059));
#56227=CARTESIAN_POINT('Ctrl Pts',(5.8894927816124,6.45952295773611,3.50431561991468));
#56228=CARTESIAN_POINT('Ctrl Pts',(5.82838302289431,6.5,3.48277674973218));
#56229=CARTESIAN_POINT('Ctrl Pts',(6.19472803466948,6.25700741281908,3.61248491411256));
#56230=CARTESIAN_POINT('Ctrl Pts',(6.4306550195388,6.26014701165697,2.7908404069676));
#56231=CARTESIAN_POINT('Ctrl Pts',(6.58110866402936,6.26293012262745,2.05835104785734));
#56232=CARTESIAN_POINT('Ctrl Pts',(6.66514060252342,6.26459431596996,1.36125860579049));
#56233=CARTESIAN_POINT('Origin',(6.177207419323,0.,0.));
#56234=CARTESIAN_POINT('Origin',(6.177207419323,0.,0.));
#56235=CARTESIAN_POINT('Ctrl Pts',(6.19472803466948,6.25700741281907,-3.61248491411259));
#56236=CARTESIAN_POINT('Ctrl Pts',(6.4306550195388,5.54701219617053,-4.02602614003637));
#56237=CARTESIAN_POINT('Ctrl Pts',(6.58472768457028,4.91347707050872,-4.39484321142696));
#56238=CARTESIAN_POINT('Ctrl Pts',(6.66935871145421,4.3102095520817,-4.74503293760454));
#56239=CARTESIAN_POINT('Origin',(6.177207419323,0.,0.));
#56240=CARTESIAN_POINT('',(6.19472803466948,-1.72045194734352E-14,-7.22496982822515));
#56241=CARTESIAN_POINT('Ctrl Pts',(6.19472803466948,-1.47104550762833E-14,
-7.22496982822515));
#56242=CARTESIAN_POINT('Ctrl Pts',(6.4306550195388,-0.71313481548644,-6.81686654700397));
#56243=CARTESIAN_POINT('Ctrl Pts',(6.58105248112949,-1.34886989409368,-6.45303961304062));
#56244=CARTESIAN_POINT('Ctrl Pts',(6.66504514382362,-1.95339415557755,-6.10593986929842));
#56245=CARTESIAN_POINT('Ctrl Pts',(6.66504514382361,1.9533941555772,-6.10593986929854));
#56246=CARTESIAN_POINT('Ctrl Pts',(6.58105248112947,1.34886989409327,-6.45303961304075));
#56247=CARTESIAN_POINT('Ctrl Pts',(6.43065501953876,0.713134815486147,-6.81686654700404));
#56248=CARTESIAN_POINT('Ctrl Pts',(6.19472803466948,-1.80411241501588E-14,
-7.22496982822515));
#56249=CARTESIAN_POINT('Origin',(6.177207419323,0.,0.));
#56250=CARTESIAN_POINT('',(6.19472803466948,-6.25700741281908,-3.61248491411256));
#56251=CARTESIAN_POINT('Ctrl Pts',(6.19472803466948,-6.25700741281908,-3.61248491411256));
#56252=CARTESIAN_POINT('Ctrl Pts',(6.4306550195388,-6.26014701165697,-2.7908404069676));
#56253=CARTESIAN_POINT('Ctrl Pts',(6.58110866402936,-6.26293012262745,-2.05835104785735));
#56254=CARTESIAN_POINT('Ctrl Pts',(6.66514060252342,-6.26459431596996,-1.3612586057905));
#56255=CARTESIAN_POINT('Ctrl Pts',(6.66935871145421,-4.31020955208199,-4.7450329376043));
#56256=CARTESIAN_POINT('Ctrl Pts',(6.58472768457026,-4.91347707050904,-4.39484321142667));
#56257=CARTESIAN_POINT('Ctrl Pts',(6.43065501953876,-5.54701219617073,-4.02602614003615));
#56258=CARTESIAN_POINT('Ctrl Pts',(6.19472803466948,-6.25700741281908,-3.61248491411256));
#56259=CARTESIAN_POINT('Origin',(6.177207419323,0.,0.));
#56260=CARTESIAN_POINT('',(6.19472803466948,-6.25700741281907,3.61248491411259));
#56261=CARTESIAN_POINT('Ctrl Pts',(6.19472803466948,-6.25700741281907,3.61248491411259));
#56262=CARTESIAN_POINT('Ctrl Pts',(6.4306550195388,-5.54701219617053,4.02602614003637));
#56263=CARTESIAN_POINT('Ctrl Pts',(6.58472768457028,-4.91347707050872,4.39484321142696));
#56264=CARTESIAN_POINT('Ctrl Pts',(6.66935871145421,-4.3102095520817,4.74503293760454));
#56265=CARTESIAN_POINT('Ctrl Pts',(6.66943768475789,-6.26442235049367,1.36025300283621));
#56266=CARTESIAN_POINT('Ctrl Pts',(6.58476982174516,-6.2627836062947,2.0577842312432));
#56267=CARTESIAN_POINT('Ctrl Pts',(6.43065501953876,-6.26014701165688,2.79084040696788));
#56268=CARTESIAN_POINT('Ctrl Pts',(6.19472803466948,-6.25700741281907,3.61248491411259));
#56269=CARTESIAN_POINT('Origin',(6.177207419323,0.,0.));
#56270=CARTESIAN_POINT('Ctrl Pts',(6.66504514382361,-1.9533941555772,6.10593986929854));
#56271=CARTESIAN_POINT('Ctrl Pts',(6.58105248112947,-1.34886989409327,6.45303961304075));
#56272=CARTESIAN_POINT('Ctrl Pts',(6.43065501953876,-0.713134815486151,
6.81686654700403));
#56273=CARTESIAN_POINT('Ctrl Pts',(6.19472803466948,1.49880108324396E-14,
7.22496982822515));
#56274=CARTESIAN_POINT('Ctrl Pts',(5.82127992530896,6.2882867881355,-3.87500942959354));
#56275=CARTESIAN_POINT('Ctrl Pts',(6.24946429650468,4.95895205574871,-4.64250119518017));
#56276=CARTESIAN_POINT('Ctrl Pts',(6.49215447047434,3.14708040407028,-5.68858578101377));
#56277=CARTESIAN_POINT('Ctrl Pts',(6.14241820370578,1.20871426115372,-6.8077019954147));
#56278=CARTESIAN_POINT('Ctrl Pts',(5.82127992530902,0.211713211864542,-7.38332081960414));
#56279=CARTESIAN_POINT('Ctrl Pts',(5.94576262842914,6.27786032969669,-3.78750125776656));
#56280=CARTESIAN_POINT('Ctrl Pts',(6.38090674377625,4.94116869510108,-4.56154066351513));
#56281=CARTESIAN_POINT('Ctrl Pts',(6.63166480681809,3.10652352931727,-5.62357322351106));
#56282=CARTESIAN_POINT('Ctrl Pts',(6.27212071493942,1.14515484589683,-6.75259524852789));
#56283=CARTESIAN_POINT('Ctrl Pts',(5.94576262842918,0.141142141243022,-7.33053715581114));
#56284=CARTESIAN_POINT('Ctrl Pts',(6.07024533154931,6.26743387125788,-3.69999308593957));
#56285=CARTESIAN_POINT('Ctrl Pts',(6.51234919104782,4.92338533445344,-4.4805801318501));
#56286=CARTESIAN_POINT('Ctrl Pts',(6.77117514316185,3.06596665456427,-5.55856066600836));
#56287=CARTESIAN_POINT('Ctrl Pts',(6.40182322617305,1.08159543063994,-6.69748850164107));
#56288=CARTESIAN_POINT('Ctrl Pts',(6.07024533154933,0.0705710706215021,
-7.27775349201815));
#56289=CARTESIAN_POINT('Ctrl Pts',(6.19472803466948,6.25700741281907,-3.61248491411259));
#56290=CARTESIAN_POINT('Ctrl Pts',(6.64379163831939,4.90560197380581,-4.39961960018506));
#56291=CARTESIAN_POINT('Ctrl Pts',(6.9106854795056,3.02540977981126,-5.49354810850567));
#56292=CARTESIAN_POINT('Ctrl Pts',(6.53152573740669,1.01803601538305,-6.64238175475426));
#56293=CARTESIAN_POINT('Ctrl Pts',(6.19472803466948,-1.80411241501588E-14,
-7.22496982822515));
#56294=CARTESIAN_POINT('',(5.82838302289405,0.233826859021164,-7.3705534994655));
#56295=CARTESIAN_POINT('Ctrl Pts',(5.82838302289405,0.23382685902116,-7.3705534994655));
#56296=CARTESIAN_POINT('Ctrl Pts',(5.88949356894673,0.194934628063732,-7.34626847480328));
#56297=CARTESIAN_POINT('Ctrl Pts',(5.95058218580015,0.156000054257608,-7.3219921646949));
#56298=CARTESIAN_POINT('Ctrl Pts',(6.07269657345378,0.0780581881388463,
-7.27346451918466));
#56299=CARTESIAN_POINT('Ctrl Pts',(6.13372433579649,0.0390496521279212,
-7.24921239235379));
#56300=CARTESIAN_POINT('Ctrl Pts',(6.19472803466948,-1.88087850445387E-14,
-7.22496982822515));
#56301=CARTESIAN_POINT('',(5.82838302289383,6.2661731409782,-3.88777674973257));
#56302=CARTESIAN_POINT('Ctrl Pts',(5.82838421256022,0.233829133738336,-7.37055218615693));
#56303=CARTESIAN_POINT('Ctrl Pts',(6.14463154721469,1.22101319990882,-6.80060119981369));
#56304=CARTESIAN_POINT('Ctrl Pts',(6.49028076601056,3.14668033196568,-5.68881676275105));
#56305=CARTESIAN_POINT('Ctrl Pts',(6.2509983619233,4.94745326120219,-4.64914002730696));
#56306=CARTESIAN_POINT('Ctrl Pts',(5.82838558568794,6.26617071740608,-3.88777814898258));
#56307=CARTESIAN_POINT('Ctrl Pts',(6.19472803466948,6.25700741281907,-3.61248491411259));
#56308=CARTESIAN_POINT('Ctrl Pts',(6.13372354963734,6.25847728208528,-3.65842477895156));
#56309=CARTESIAN_POINT('Ctrl Pts',(6.07269500050242,6.25997599169669,-3.70433381675495));
#56310=CARTESIAN_POINT('Ctrl Pts',(5.9505806116696,6.26303123391776,-3.796097273956));
#56311=CARTESIAN_POINT('Ctrl Pts',(5.88949278161014,6.26458782859284,-3.84195316777262));
#56312=CARTESIAN_POINT('Ctrl Pts',(5.82838302289431,6.26617314097787,-3.88777674973276));
#56313=CARTESIAN_POINT('Origin',(6.8,0.,-1.11022302462516E-15));
#56314=CARTESIAN_POINT('',(6.8,-4.37,5.35170651227393E-16));
#56315=CARTESIAN_POINT('Origin',(6.8,0.,0.));
#56316=CARTESIAN_POINT('Origin',(5.82838302289405,6.5,-3.4827767497333));
#56317=CARTESIAN_POINT('',(5.82838302289387,6.5,-3.48277674973257));
#56318=CARTESIAN_POINT('Origin',(6.19472803466948,-1.72045194734352E-14,
-7.22496982822515));
#56319=CARTESIAN_POINT('',(5.82838302289383,-0.2338268590218,-7.37055349946514));
#56320=CARTESIAN_POINT('Ctrl Pts',(6.19472803466948,-1.39959883312281E-14,
-7.22496982822515));
#56321=CARTESIAN_POINT('Ctrl Pts',(6.13372354964118,-0.0390501553614202,
-7.24921270476789));
#56322=CARTESIAN_POINT('Ctrl Pts',(6.07269500051012,-0.0780591935542958,
-7.27346514426443));
#56323=CARTESIAN_POINT('Ctrl Pts',(5.95058061167065,-0.156001057523206,
-7.32199279024577));
#56324=CARTESIAN_POINT('Ctrl Pts',(5.88949278161218,-0.194935129143466,
-7.3462687876857));
#56325=CARTESIAN_POINT('Ctrl Pts',(5.82838302289431,-0.233826859022136,
-7.37055349946494));
#56326=CARTESIAN_POINT('',(5.82838302289387,0.233826859021797,-7.37055349946514));
#56327=CARTESIAN_POINT('Origin',(5.82838302289405,6.26617314097884,3.8877767497322));
#56328=CARTESIAN_POINT('',(5.82838302289387,6.2661731409782,3.88777674973257));
#56329=CARTESIAN_POINT('Origin',(6.19472803466948,-6.25700741281908,-3.61248491411256));
#56330=CARTESIAN_POINT('',(5.82838302289405,-6.26617314097884,-3.8877767497322));
#56331=CARTESIAN_POINT('Ctrl Pts',(5.82838302289405,-6.26617314097884,-3.8877767497322));
#56332=CARTESIAN_POINT('Ctrl Pts',(5.88949356895342,-6.26458780816836,-3.84195257737708));
#56333=CARTESIAN_POINT('Ctrl Pts',(5.95058218580324,-6.26303119380752,-3.79609609232396));
#56334=CARTESIAN_POINT('Ctrl Pts',(6.07269657345032,-6.25997595306935,-3.70433263349656));
#56335=CARTESIAN_POINT('Ctrl Pts',(6.13372433579501,-6.25847726314342,-3.65842418692974));
#56336=CARTESIAN_POINT('Ctrl Pts',(6.19472803466948,-6.25700741281908,-3.61248491411257));
#56337=CARTESIAN_POINT('',(5.82838302289383,-6.5,-3.48277674973257));
#56338=CARTESIAN_POINT('Ctrl Pts',(6.19472803466948,-6.25700741281908,-3.61248491411257));
#56339=CARTESIAN_POINT('Ctrl Pts',(6.13372354964143,-6.29752743744644,-3.59078792581931));
#56340=CARTESIAN_POINT('Ctrl Pts',(6.07269500051088,-6.33803518525029,-3.56913132751554));
#56341=CARTESIAN_POINT('Ctrl Pts',(5.95058061166937,-6.41903229144179,-3.5258955162901));
#56342=CARTESIAN_POINT('Ctrl Pts',(5.88949278160931,-6.45952295773815,-3.5043156199136));
#56343=CARTESIAN_POINT('Ctrl Pts',(5.82838302289431,-6.5,-3.48277674973218));
#56344=CARTESIAN_POINT('',(5.82838302289387,-6.2661731409782,-3.88777674973257));
#56345=CARTESIAN_POINT('Origin',(5.82838302289405,-0.233826859021165,7.3705534994655));
#56346=CARTESIAN_POINT('',(5.82838302289405,-0.233826859021165,7.3705534994655));
#56347=CARTESIAN_POINT('',(5.82838302289388,-0.233826859021798,7.37055349946514));
#56348=CARTESIAN_POINT('Ctrl Pts',(5.82838302289405,-0.233826859021165,
7.3705534994655));
#56349=CARTESIAN_POINT('Ctrl Pts',(5.88949356895343,-0.194934628059473,
7.34626847480061));
#56350=CARTESIAN_POINT('Ctrl Pts',(5.95058218580337,-0.156000054255553,
7.32199216469362));
#56351=CARTESIAN_POINT('Ctrl Pts',(6.07269657344927,-0.0780581881417256,
7.27346451918645));
#56352=CARTESIAN_POINT('Ctrl Pts',(6.13372433579441,-0.0390496521292542,
7.24921239235461));
#56353=CARTESIAN_POINT('Ctrl Pts',(6.19472803466949,1.16722608064283E-14,
7.22496982822515));
#56354=CARTESIAN_POINT('Origin',(6.19472803466948,-6.25700741281907,3.61248491411259));
#56355=CARTESIAN_POINT('',(5.82838302289405,-6.5,3.4827767497333));
#56356=CARTESIAN_POINT('Ctrl Pts',(5.82838302289405,-6.5,3.4827767497333));
#56357=CARTESIAN_POINT('Ctrl Pts',(5.88949356894732,-6.45952243623187,3.50431589742138));
#56358=CARTESIAN_POINT('Ctrl Pts',(5.95058218580049,-6.41903124806498,3.52589607236873));
#56359=CARTESIAN_POINT('Ctrl Pts',(6.07269657345065,-6.33803414121018,3.56913188568959));
#56360=CARTESIAN_POINT('Ctrl Pts',(6.13372433579476,-6.29752691527246,3.59078820542455));
#56361=CARTESIAN_POINT('Ctrl Pts',(6.19472803466948,-6.25700741281907,3.61248491411259));
#56362=CARTESIAN_POINT('',(5.82838302289383,-6.2661731409782,3.88777674973257));
#56363=CARTESIAN_POINT('Ctrl Pts',(6.19472803466948,-6.25700741281907,3.61248491411259));
#56364=CARTESIAN_POINT('Ctrl Pts',(6.13372354964038,-6.25847728208521,3.65842477894927));
#56365=CARTESIAN_POINT('Ctrl Pts',(6.07269500050845,-6.25997599169654,3.70433381675042));
#56366=CARTESIAN_POINT('Ctrl Pts',(5.95058061166901,-6.26303123391778,3.79609727395645));
#56367=CARTESIAN_POINT('Ctrl Pts',(5.88949278160903,-6.26458782859287,3.84195316777345));
#56368=CARTESIAN_POINT('Ctrl Pts',(5.82838302289431,-6.26617314097787,3.88777674973276));
#56369=CARTESIAN_POINT('',(5.82838302289387,-6.5,3.48277674973257));
#56370=CARTESIAN_POINT('Ctrl Pts',(5.82127992530897,-6.2882867881355,3.87500942959354));
#56371=CARTESIAN_POINT('Ctrl Pts',(6.24946429650468,-4.95895205574871,4.64250119518017));
#56372=CARTESIAN_POINT('Ctrl Pts',(6.49215447047434,-3.14708040407028,5.68858578101376));
#56373=CARTESIAN_POINT('Ctrl Pts',(6.14241820370578,-1.20871426115372,6.8077019954147));
#56374=CARTESIAN_POINT('Ctrl Pts',(5.82127992530902,-0.211713211864546,
7.38332081960414));
#56375=CARTESIAN_POINT('Ctrl Pts',(5.94576262842914,-6.27786032969669,3.78750125776656));
#56376=CARTESIAN_POINT('Ctrl Pts',(6.38090674377625,-4.94116869510108,4.56154066351513));
#56377=CARTESIAN_POINT('Ctrl Pts',(6.63166480681809,-3.10652352931728,5.62357322351106));
#56378=CARTESIAN_POINT('Ctrl Pts',(6.27212071493942,-1.14515484589683,6.75259524852789));
#56379=CARTESIAN_POINT('Ctrl Pts',(5.94576262842918,-0.141142141243025,
7.33053715581114));
#56380=CARTESIAN_POINT('Ctrl Pts',(6.07024533154931,-6.26743387125788,3.69999308593957));
#56381=CARTESIAN_POINT('Ctrl Pts',(6.51234919104782,-4.92338533445345,4.4805801318501));
#56382=CARTESIAN_POINT('Ctrl Pts',(6.77117514316185,-3.06596665456427,5.55856066600836));
#56383=CARTESIAN_POINT('Ctrl Pts',(6.40182322617305,-1.08159543063994,6.69748850164107));
#56384=CARTESIAN_POINT('Ctrl Pts',(6.07024533154933,-0.0705710706215052,
7.27775349201815));
#56385=CARTESIAN_POINT('Ctrl Pts',(6.19472803466948,-6.25700741281907,3.61248491411259));
#56386=CARTESIAN_POINT('Ctrl Pts',(6.64379163831939,-4.90560197380581,4.39961960018506));
#56387=CARTESIAN_POINT('Ctrl Pts',(6.9106854795056,-3.02540977981126,5.49354810850567));
#56388=CARTESIAN_POINT('Ctrl Pts',(6.53152573740669,-1.01803601538306,6.64238175475426));
#56389=CARTESIAN_POINT('Ctrl Pts',(6.19472803466948,1.49880108324396E-14,
7.22496982822515));
#56390=CARTESIAN_POINT('Ctrl Pts',(5.82838421256021,-0.233829133738338,
7.37055218615693));
#56391=CARTESIAN_POINT('Ctrl Pts',(6.14463154721469,-1.22101319990882,6.80060119981369));
#56392=CARTESIAN_POINT('Ctrl Pts',(6.49028076601056,-3.14668033196568,5.68881676275105));
#56393=CARTESIAN_POINT('Ctrl Pts',(6.2509983619233,-4.9474532612022,4.64914002730695));
#56394=CARTESIAN_POINT('Ctrl Pts',(5.82838558568794,-6.26617071740609,3.88777814898258));
#56395=CARTESIAN_POINT('Origin',(0.,-6.3830865704891,3.68527674973257));
#56396=CARTESIAN_POINT('',(0.691578435026327,-6.2661731409782,3.88777674973257));
#56397=CARTESIAN_POINT('',(0.691578435026392,-6.5,3.48277674973257));
#56398=CARTESIAN_POINT('Ctrl Pts',(0.691578435026327,-6.2661731409782,3.88777674973257));
#56399=CARTESIAN_POINT('Ctrl Pts',(0.687292182208882,-6.3830865704891,3.68527674973257));
#56400=CARTESIAN_POINT('Ctrl Pts',(0.691578435026392,-6.5,3.48277674973257));
#56401=CARTESIAN_POINT('',(0.,-6.5,3.48277674973257));
#56402=CARTESIAN_POINT('',(0.,-6.2661731409782,3.88777674973257));
#56403=CARTESIAN_POINT('Ctrl Pts',(5.82127992530897,-6.5,-3.50831139001062));
#56404=CARTESIAN_POINT('Ctrl Pts',(6.14241820370575,-6.5,-2.35707374163068));
#56405=CARTESIAN_POINT('Ctrl Pts',(6.49243586254982,-6.5,-0.118785051139954));
#56406=CARTESIAN_POINT('Ctrl Pts',(6.2494642965047,-6.5,1.97332785883873));
#56407=CARTESIAN_POINT('Ctrl Pts',(5.82127992530902,-6.5,3.50831139001058));
#56408=CARTESIAN_POINT('Ctrl Pts',(5.94576262842914,-6.41900247093969,-3.5430358980446));
#56409=CARTESIAN_POINT('Ctrl Pts',(6.27212071493947,-6.4204964496477,-2.38456443644943));
#56410=CARTESIAN_POINT('Ctrl Pts',(6.63194145333222,-6.42341735463559,-0.121399944768473));
#56411=CARTESIAN_POINT('Ctrl Pts',(6.38090674377616,-6.42099444255032,1.99840728258572));
#56412=CARTESIAN_POINT('Ctrl Pts',(5.94576262842918,-6.41900247093969,3.54303589804458));
#56413=CARTESIAN_POINT('Ctrl Pts',(6.07024533154931,-6.33800494187939,-3.57776040607858));
#56414=CARTESIAN_POINT('Ctrl Pts',(6.40182322617319,-6.3409928992954,-2.41205513126818));
#56415=CARTESIAN_POINT('Ctrl Pts',(6.77144704411462,-6.34683470927118,-0.124014838396995));
#56416=CARTESIAN_POINT('Ctrl Pts',(6.51234919104763,-6.34198888510063,2.02348670633271));
#56417=CARTESIAN_POINT('Ctrl Pts',(6.07024533154933,-6.33800494187938,3.57776040607859));
#56418=CARTESIAN_POINT('Ctrl Pts',(6.19472803466948,-6.25700741281908,-3.61248491411256));
#56419=CARTESIAN_POINT('Ctrl Pts',(6.53152573740691,-6.2614893489431,-2.43954582608693));
#56420=CARTESIAN_POINT('Ctrl Pts',(6.91095263489701,-6.27025206390677,-0.126629732025515));
#56421=CARTESIAN_POINT('Ctrl Pts',(6.64379163831909,-6.26298332765095,2.0485661300797));
#56422=CARTESIAN_POINT('Ctrl Pts',(6.19472803466948,-6.25700741281907,3.61248491411259));
#56423=CARTESIAN_POINT('Ctrl Pts',(5.82838560050068,-6.5,3.48277395419486));
#56424=CARTESIAN_POINT('Ctrl Pts',(6.25100014187621,-6.5,1.96005055047028));
#56425=CARTESIAN_POINT('Ctrl Pts',(6.49056037813313,-6.5,-0.119247370498952));
#56426=CARTESIAN_POINT('Ctrl Pts',(6.14463332716764,-6.5,-2.34287179454352));
#56427=CARTESIAN_POINT('Ctrl Pts',(5.82838423229859,-6.5,-3.48277411916905));
#56428=CARTESIAN_POINT('Origin',(0.,5.3776427755281E-16,7.37055349946514));
#56429=CARTESIAN_POINT('',(0.691578435026327,0.233826859021798,7.37055349946513));
#56430=CARTESIAN_POINT('',(0.691578435026391,-0.233826859021798,7.37055349946514));
#56431=CARTESIAN_POINT('Ctrl Pts',(0.691578435026327,0.233826859021798,
7.37055349946513));
#56432=CARTESIAN_POINT('Ctrl Pts',(0.687292182208882,3.78169717762944E-15,
7.37055349946514));
#56433=CARTESIAN_POINT('Ctrl Pts',(0.691578435026391,-0.233826859021798,
7.37055349946514));
#56434=CARTESIAN_POINT('',(0.,-0.233826859021798,7.37055349946514));
#56435=CARTESIAN_POINT('',(0.,0.233826859021799,7.37055349946514));
#56436=CARTESIAN_POINT('Origin',(0.,-6.3830865704891,-3.68527674973257));
#56437=CARTESIAN_POINT('',(0.691578435026327,-6.5,-3.48277674973257));
#56438=CARTESIAN_POINT('',(0.691578435026391,-6.2661731409782,-3.88777674973257));
#56439=CARTESIAN_POINT('Ctrl Pts',(0.691578435026327,-6.5,-3.48277674973257));
#56440=CARTESIAN_POINT('Ctrl Pts',(0.687292182208882,-6.38308657048911,
-3.68527674973256));
#56441=CARTESIAN_POINT('Ctrl Pts',(0.691578435026391,-6.2661731409782,-3.88777674973257));
#56442=CARTESIAN_POINT('',(0.,-6.2661731409782,-3.88777674973257));
#56443=CARTESIAN_POINT('',(0.,-6.5,-3.48277674973257));
#56444=CARTESIAN_POINT('Ctrl Pts',(5.82127992530897,-0.211713211864505,
-7.38332081960416));
#56445=CARTESIAN_POINT('Ctrl Pts',(6.14241820370575,-1.20871426115459,-6.80770199541419));
#56446=CARTESIAN_POINT('Ctrl Pts',(6.49215447047434,-3.14708040407219,-5.68858578101266));
#56447=CARTESIAN_POINT('Ctrl Pts',(6.2494642965047,-4.95895205574989,-4.64250119517949));
#56448=CARTESIAN_POINT('Ctrl Pts',(5.82127992530902,-6.28828678813546,-3.87500942959356));
#56449=CARTESIAN_POINT('Ctrl Pts',(5.94576262842914,-0.141142141243009,
-7.33053715581116));
#56450=CARTESIAN_POINT('Ctrl Pts',(6.27212071493947,-1.14515484589772,-6.75259524852742));
#56451=CARTESIAN_POINT('Ctrl Pts',(6.63166480681812,-3.1065235293192,-5.62357322350997));
#56452=CARTESIAN_POINT('Ctrl Pts',(6.38090674377616,-4.94116869510222,-4.56154066351441));
#56453=CARTESIAN_POINT('Ctrl Pts',(5.94576262842917,-6.27786032969667,-3.78750125776656));
#56454=CARTESIAN_POINT('Ctrl Pts',(6.07024533154931,-0.0705710706215116,
-7.27775349201816));
#56455=CARTESIAN_POINT('Ctrl Pts',(6.40182322617319,-1.08159543064085,-6.69748850164065));
#56456=CARTESIAN_POINT('Ctrl Pts',(6.7711751431619,-3.06596665456621,-5.55856066600728));
#56457=CARTESIAN_POINT('Ctrl Pts',(6.51234919104763,-4.92338533445454,-4.48058013184934));
#56458=CARTESIAN_POINT('Ctrl Pts',(6.07024533154933,-6.26743387125788,-3.69999308593956));
#56459=CARTESIAN_POINT('Ctrl Pts',(6.19472803466948,-1.47104550762833E-14,
-7.22496982822515));
#56460=CARTESIAN_POINT('Ctrl Pts',(6.53152573740691,-1.01803601538398,-6.64238175475387));
#56461=CARTESIAN_POINT('Ctrl Pts',(6.91068547950568,-3.02540977981322,-5.49354810850458));
#56462=CARTESIAN_POINT('Ctrl Pts',(6.64379163831909,-4.90560197380687,-4.39961960018427));
#56463=CARTESIAN_POINT('Ctrl Pts',(6.19472803466948,-6.25700741281908,-3.61248491411256));
#56464=CARTESIAN_POINT('Ctrl Pts',(5.82838558568782,-6.26617071740664,-3.88777814898226));
#56465=CARTESIAN_POINT('Ctrl Pts',(6.25099836192328,-4.94745326120368,-4.6491400273061));
#56466=CARTESIAN_POINT('Ctrl Pts',(6.49028076601057,-3.14668033196789,-5.68881676274977));
#56467=CARTESIAN_POINT('Ctrl Pts',(6.14463154721472,-1.22101319991002,-6.800601199813));
#56468=CARTESIAN_POINT('Ctrl Pts',(5.82838421256034,-0.233829133738889,
-7.37055218615661));
#56469=CARTESIAN_POINT('Origin',(0.,6.3830865704891,3.68527674973257));
#56470=CARTESIAN_POINT('',(0.691578435026327,6.5,3.48277674973257));
#56471=CARTESIAN_POINT('',(0.691578435026392,6.2661731409782,3.88777674973257));
#56472=CARTESIAN_POINT('Ctrl Pts',(0.691578435026327,6.5,3.48277674973257));
#56473=CARTESIAN_POINT('Ctrl Pts',(0.687292182208883,6.3830865704891,3.68527674973256));
#56474=CARTESIAN_POINT('Ctrl Pts',(0.691578435026392,6.2661731409782,3.88777674973257));
#56475=CARTESIAN_POINT('',(0.,6.2661731409782,3.88777674973257));
#56476=CARTESIAN_POINT('',(0.,6.5,3.48277674973257));
#56477=CARTESIAN_POINT('Origin',(0.,-1.23165366794353E-15,-7.37055349946514));
#56478=CARTESIAN_POINT('',(0.691578435026327,-0.233826859021799,-7.37055349946513));
#56479=CARTESIAN_POINT('',(0.691578435026391,0.233826859021797,-7.37055349946514));
#56480=CARTESIAN_POINT('Ctrl Pts',(0.691578435026327,-0.233826859021799,
-7.37055349946513));
#56481=CARTESIAN_POINT('Ctrl Pts',(0.687292182208882,-4.44089209850063E-15,
-7.37055349946514));
#56482=CARTESIAN_POINT('Ctrl Pts',(0.691578435026391,0.233826859021797,
-7.37055349946514));
#56483=CARTESIAN_POINT('',(0.,0.233826859021797,-7.37055349946514));
#56484=CARTESIAN_POINT('',(0.,-0.2338268590218,-7.37055349946514));
#56485=CARTESIAN_POINT('Origin',(0.,6.3830865704891,-3.68527674973257));
#56486=CARTESIAN_POINT('',(0.691578435026327,6.2661731409782,-3.88777674973257));
#56487=CARTESIAN_POINT('',(0.691578435026391,6.5,-3.48277674973257));
#56488=CARTESIAN_POINT('Ctrl Pts',(0.691578435026327,6.2661731409782,-3.88777674973257));
#56489=CARTESIAN_POINT('Ctrl Pts',(0.687292182208882,6.3830865704891,-3.68527674973257));
#56490=CARTESIAN_POINT('Ctrl Pts',(0.691578435026391,6.5,-3.48277674973257));
#56491=CARTESIAN_POINT('',(0.,6.5,-3.48277674973257));
#56492=CARTESIAN_POINT('',(0.,6.2661731409782,-3.88777674973257));
#56493=CARTESIAN_POINT('Origin',(0.,6.5,3.75277674973257));
#56494=CARTESIAN_POINT('Ctrl Pts',(0.691578435026392,6.2661731409782,3.88777674973257));
#56495=CARTESIAN_POINT('Ctrl Pts',(-0.259333426979357,3.2499999999987,5.62916512459961));
#56496=CARTESIAN_POINT('Ctrl Pts',(0.691578435026327,0.233826859021798,
7.37055349946514));
#56497=CARTESIAN_POINT('Origin',(0.,6.5,-3.75277674973257));
#56498=CARTESIAN_POINT('Ctrl Pts',(0.691578435026391,6.5,-3.48277674973257));
#56499=CARTESIAN_POINT('Ctrl Pts',(-0.259333426979358,6.5,1.50435219836709E-12));
#56500=CARTESIAN_POINT('Ctrl Pts',(0.691578435026327,6.5,3.48277674973257));
#56501=CARTESIAN_POINT('Origin',(0.,-1.37874781034238E-15,-7.50555349946513));
#56502=CARTESIAN_POINT('Ctrl Pts',(0.691578435026391,0.233826859021797,
-7.37055349946514));
#56503=CARTESIAN_POINT('Ctrl Pts',(-0.259333426979357,3.2500000000013,-5.6291651245981));
#56504=CARTESIAN_POINT('Ctrl Pts',(0.691578435026327,6.2661731409782,-3.88777674973257));
#56505=CARTESIAN_POINT('Origin',(0.622792580677002,0.,0.));
#56506=CARTESIAN_POINT('',(0.,-6.17797863635533,7.56584176221328E-16));
#56507=CARTESIAN_POINT('Origin',(0.,0.,0.));
#56508=CARTESIAN_POINT('',(0.186162505632566,-6.5,-1.05927327362393E-15));
#56509=CARTESIAN_POINT('',(0.622792580677002,-7.25527674973257,-8.8851514484882E-16));
#56510=CARTESIAN_POINT('Ctrl Pts',(0.691578435026392,-6.5,3.48277674973257));
#56511=CARTESIAN_POINT('Ctrl Pts',(0.186162505632697,-6.5,1.63165792561282));
#56512=CARTESIAN_POINT('Ctrl Pts',(0.186162505632566,-6.5,-1.32252612780209E-15));
#56513=CARTESIAN_POINT('Ctrl Pts',(0.691578435026392,-0.233826859021798,
7.37055349946514));
#56514=CARTESIAN_POINT('Ctrl Pts',(-0.259333426979358,-3.2500000000013,
5.6291651245981));
#56515=CARTESIAN_POINT('Ctrl Pts',(0.691578435026327,-6.2661731409782,3.88777674973257));
#56516=CARTESIAN_POINT('Ctrl Pts',(0.691578435026391,-6.2661731409782,-3.88777674973257));
#56517=CARTESIAN_POINT('Ctrl Pts',(-0.25933342697936,-3.2499999999987,-5.6291651245996));
#56518=CARTESIAN_POINT('Ctrl Pts',(0.691578435026327,-0.233826859021799,
-7.37055349946513));
#56519=CARTESIAN_POINT('Ctrl Pts',(0.186162505632566,-6.5,-1.32252612780209E-15));
#56520=CARTESIAN_POINT('Ctrl Pts',(0.186162505632435,-6.5,-1.63165792561357));
#56521=CARTESIAN_POINT('Ctrl Pts',(0.691578435026327,-6.5,-3.48277674973257));
#56522=CARTESIAN_POINT('Origin',(0.15,0.,0.));
#56523=CARTESIAN_POINT('',(0.,-4.37,-5.35170651227393E-16));
#56524=CARTESIAN_POINT('Origin',(0.,0.,0.));
#56525=CARTESIAN_POINT('',(0.4,-4.05,-4.95981953654678E-16));
#56526=CARTESIAN_POINT('',(0.15,-4.25,-5.20474889637625E-16));
#56527=CARTESIAN_POINT('Origin',(0.4,0.,0.));
#56528=CARTESIAN_POINT('Origin',(3.4,0.,0.));
#56529=CARTESIAN_POINT('',(6.4,-4.05,-4.95981953654678E-16));
#56530=CARTESIAN_POINT('',(3.4,-4.05,-4.95981953654678E-16));
#56531=CARTESIAN_POINT('Origin',(6.4,0.,0.));
#56532=CARTESIAN_POINT('Origin',(6.65,0.,0.));
#56533=CARTESIAN_POINT('',(6.65,-4.25,-5.20474889637625E-16));
#56534=CARTESIAN_POINT('Origin',(0.,-6.5,-3.75277674973257));
#56535=CARTESIAN_POINT('Origin',(0.,-6.5,3.75277674973257));
#56536=CARTESIAN_POINT('Origin',(0.,4.5958260344746E-16,7.50555349946513));
#56537=CARTESIAN_POINT('Origin',(0.,0.,-1.11022302462516E-15));
#56616=UNCERTAINTY_MEASURE_WITH_UNIT(LENGTH_MEASURE(0.01),#56640,
'DISTANCE_ACCURACY_VALUE',
'Maximum model space distance between geometric entities at asserted c
onnectivities');
#56617=UNCERTAINTY_MEASURE_WITH_UNIT(LENGTH_MEASURE(0.01),#56640,
'DISTANCE_ACCURACY_VALUE',
'Maximum model space distance between geometric entities at asserted c
onnectivities');
#56638=(
GEOMETRIC_REPRESENTATION_CONTEXT(3)
GLOBAL_UNCERTAINTY_ASSIGNED_CONTEXT((#56616))
GLOBAL_UNIT_ASSIGNED_CONTEXT((#56640,#56642,#56643))
REPRESENTATION_CONTEXT('','3D')
);
#56639=(
GEOMETRIC_REPRESENTATION_CONTEXT(3)
GLOBAL_UNCERTAINTY_ASSIGNED_CONTEXT((#56617))
GLOBAL_UNIT_ASSIGNED_CONTEXT((#56640,#56642,#56643))
REPRESENTATION_CONTEXT('','3D')
);
#56640=(
LENGTH_UNIT()
NAMED_UNIT(*)
SI_UNIT(.MILLI.,.METRE.)
);
#56642=(
NAMED_UNIT(*)
PLANE_ANGLE_UNIT()
SI_UNIT($,.RADIAN.)
);
#56643=(
NAMED_UNIT(*)
SI_UNIT($,.STERADIAN.)
SOLID_ANGLE_UNIT()
);
#56664=SHAPE_DEFINITION_REPRESENTATION(#56685,#56764);
#56685=PRODUCT_DEFINITION_SHAPE('',$,#56786);
#56764=SHAPE_REPRESENTATION('',(#18687),#56638);
#56765=PRODUCT_DEFINITION_CONTEXT('part definition',#56830,'design');
#56786=PRODUCT_DEFINITION('2026-10-26-00-02-54-694',
'17_Hex_Nut_ISO_4032_M8',#56807,#56765);
#56807=PRODUCT_DEFINITION_FORMATION('',$,#56852);
#56830=APPLICATION_CONTEXT(
'Core Data for Automotive Mechanical Design Process');
#56831=PRODUCT_CONTEXT('part definition',#56830,'mechanical');
#56852=PRODUCT('2026-10-26-00-02-54-694','17_Hex_Nut_ISO_4032_M8',$,(#56831));
#56916=COLOUR_RGB('Black',0.12,0.14,0.17);
#56917=FILL_AREA_STYLE_COLOUR('',#56916);
#56918=FILL_AREA_STYLE('',(#56917));
#56919=SURFACE_STYLE_FILL_AREA(#56918);
#56920=SURFACE_SIDE_STYLE('',(#56919));
#56921=SURFACE_STYLE_USAGE(.BOTH.,#56920);
#56922=PRESENTATION_STYLE_ASSIGNMENT((#56921));
ENDSEC;
END-ISO-10303-21;
